ISO-10303-21;
HEADER;
/* Generated by software containing ST-Developer
 * from STEP Tools, Inc. (www.steptools.com) 
 */

FILE_DESCRIPTION(
/* description */ ('Independent bearing-supported roller-ramp one-way clutch. Six logarit
hmic ramps with plain solid rollers, sprung guided plungers, native Co
il variants, removable shared keepers, rounded parallel key, shaft wit
h complete retaining lips, bronze journal/thrust support and bolted co
vers. Native rotor, roller planar/spin and plunger joints permit manua
l geometric engaged/released inspection. Automatic frictional torque s
witching/contact dynamics are not simulated; no capacity, hardness, fi
t, lubrication, speed, force or life rating. External input driver/cou
pling/anchors outside assembly.'),
/* implementation_level */ '2;1');

FILE_NAME(
/* name */ 'Countersunk screw M3x6.step',
/* time_stamp */ '2026-11-08T07:04:38-08:00',
/* author */ (''),
/* organization */ (''),
/* preprocessor_version */ 'ST-DEVELOPER v20.2',
/* originating_system */ 'Autodesk Translation Framework v15.17.0.0',
/* authorisation */ '');

FILE_SCHEMA (('AUTOMOTIVE_DESIGN { 1 0 10303 214 3 1 1 }'));
ENDSEC;

DATA;
#10=MECHANICAL_DESIGN_GEOMETRIC_PRESENTATION_REPRESENTATION('',(#315),#99526);
#254=CONICAL_SURFACE('',#19720,1.25,0.785398163397449);
#255=CONICAL_SURFACE('',#19738,2.25,0.785398163397448);
#283=SHAPE_REPRESENTATION_RELATIONSHIP('SRR','None',#99640,#299);
#299=ADVANCED_BREP_SHAPE_REPRESENTATION('',(#331),#99525);
#315=STYLED_ITEM('',(#99725),#331);
#331=MANIFOLD_SOLID_BREP('Body1',#18285);
#439=FACE_BOUND('',#2774,.T.);
#604=PLANE('',#19725);
#605=PLANE('',#19726);
#606=PLANE('',#19727);
#607=PLANE('',#19728);
#608=PLANE('',#19729);
#609=PLANE('',#19730);
#610=PLANE('',#19731);
#611=PLANE('',#19732);
#612=PLANE('',#19736);
#613=PLANE('',#19739);
#673=B_SPLINE_SURFACE_WITH_KNOTS('',3,3,((#98697,#98698,#98699,#98700,#98701,
#98702,#98703,#98704,#98705,#98706,#98707,#98708,#98709,#98710,#98711,#98712,
#98713,#98714,#98715,#98716,#98717,#98718,#98719,#98720,#98721,#98722,#98723,
#98724,#98725,#98726,#98727,#98728,#98729,#98730,#98731,#98732,#98733,#98734,
#98735,#98736,#98737,#98738,#98739,#98740,#98741,#98742,#98743,#98744,#98745,
#98746,#98747,#98748,#98749,#98750,#98751,#98752,#98753),(#98754,#98755,
#98756,#98757,#98758,#98759,#98760,#98761,#98762,#98763,#98764,#98765,#98766,
#98767,#98768,#98769,#98770,#98771,#98772,#98773,#98774,#98775,#98776,#98777,
#98778,#98779,#98780,#98781,#98782,#98783,#98784,#98785,#98786,#98787,#98788,
#98789,#98790,#98791,#98792,#98793,#98794,#98795,#98796,#98797,#98798,#98799,
#98800,#98801,#98802,#98803,#98804,#98805,#98806,#98807,#98808,#98809,#98810),
(#98811,#98812,#98813,#98814,#98815,#98816,#98817,#98818,#98819,#98820,
#98821,#98822,#98823,#98824,#98825,#98826,#98827,#98828,#98829,#98830,#98831,
#98832,#98833,#98834,#98835,#98836,#98837,#98838,#98839,#98840,#98841,#98842,
#98843,#98844,#98845,#98846,#98847,#98848,#98849,#98850,#98851,#98852,#98853,
#98854,#98855,#98856,#98857,#98858,#98859,#98860,#98861,#98862,#98863,#98864,
#98865,#98866,#98867),(#98868,#98869,#98870,#98871,#98872,#98873,#98874,
#98875,#98876,#98877,#98878,#98879,#98880,#98881,#98882,#98883,#98884,#98885,
#98886,#98887,#98888,#98889,#98890,#98891,#98892,#98893,#98894,#98895,#98896,
#98897,#98898,#98899,#98900,#98901,#98902,#98903,#98904,#98905,#98906,#98907,
#98908,#98909,#98910,#98911,#98912,#98913,#98914,#98915,#98916,#98917,#98918,
#98919,#98920,#98921,#98922,#98923,#98924)),.UNSPECIFIED.,.F.,.F.,.F.,(4,
4),(4,1,1,1,1,1,1,1,1,1,1,1,1,1,1,1,1,1,1,1,1,1,1,1,1,1,1,1,1,1,1,1,1,1,
1,1,1,1,1,1,1,1,1,1,1,1,1,1,1,1,1,1,1,1,4),(0.,0.0329955678841871),(11.6159397475004,
12.6132790597317,13.610618371963,14.6079576841943,15.6052969964256,16.6026363086569,
17.5999756208882,18.5973149331195,19.5946542453507,20.591993557582,21.5893328698133,
22.5866721820446,23.5840114942759,24.5813508065072,25.5786901187385,26.5760294309698,
27.5733687432011,28.5707080554324,29.5680473676637,30.565386679895,31.5627259921263,
32.5600653043576,33.5574046165888,34.5547439288201,35.5520832410514,36.5494225532827,
37.546761865514,38.5441011777453,39.5414404899766,40.5387798022079,41.5361191144392,
42.5334584266705,43.5307977389018,44.5281370511331,45.5254763633644,46.5228156755957,
47.520154987827,48.5174943000582,49.5148336122895,50.5121729245208,51.5095122367521,
52.5068515489834,53.5041908612147,54.501530173446,55.4988694856773,56.4962087979086,
57.4935481101399,58.4908874223712,59.4882267346025,60.4855660468338,61.4829053590651,
62.4802446712963,63.4775839835276,64.4749232957589,65.4722626079902),
 .UNSPECIFIED.);
#674=B_SPLINE_SURFACE_WITH_KNOTS('',3,3,((#99081,#99082,#99083,#99084,#99085,
#99086,#99087,#99088,#99089,#99090,#99091,#99092,#99093,#99094,#99095,#99096,
#99097,#99098,#99099,#99100,#99101,#99102,#99103,#99104,#99105,#99106,#99107,
#99108,#99109,#99110,#99111,#99112,#99113,#99114,#99115,#99116,#99117,#99118,
#99119,#99120,#99121,#99122,#99123,#99124,#99125,#99126,#99127,#99128,#99129,
#99130,#99131,#99132,#99133,#99134,#99135,#99136,#99137,#99138,#99139),
(#99140,#99141,#99142,#99143,#99144,#99145,#99146,#99147,#99148,#99149,
#99150,#99151,#99152,#99153,#99154,#99155,#99156,#99157,#99158,#99159,#99160,
#99161,#99162,#99163,#99164,#99165,#99166,#99167,#99168,#99169,#99170,#99171,
#99172,#99173,#99174,#99175,#99176,#99177,#99178,#99179,#99180,#99181,#99182,
#99183,#99184,#99185,#99186,#99187,#99188,#99189,#99190,#99191,#99192,#99193,
#99194,#99195,#99196,#99197,#99198),(#99199,#99200,#99201,#99202,#99203,
#99204,#99205,#99206,#99207,#99208,#99209,#99210,#99211,#99212,#99213,#99214,
#99215,#99216,#99217,#99218,#99219,#99220,#99221,#99222,#99223,#99224,#99225,
#99226,#99227,#99228,#99229,#99230,#99231,#99232,#99233,#99234,#99235,#99236,
#99237,#99238,#99239,#99240,#99241,#99242,#99243,#99244,#99245,#99246,#99247,
#99248,#99249,#99250,#99251,#99252,#99253,#99254,#99255,#99256,#99257),
(#99258,#99259,#99260,#99261,#99262,#99263,#99264,#99265,#99266,#99267,
#99268,#99269,#99270,#99271,#99272,#99273,#99274,#99275,#99276,#99277,#99278,
#99279,#99280,#99281,#99282,#99283,#99284,#99285,#99286,#99287,#99288,#99289,
#99290,#99291,#99292,#99293,#99294,#99295,#99296,#99297,#99298,#99299,#99300,
#99301,#99302,#99303,#99304,#99305,#99306,#99307,#99308,#99309,#99310,#99311,
#99312,#99313,#99314,#99315,#99316)),.UNSPECIFIED.,.F.,.F.,.F.,(4,4),(4,
1,1,1,1,1,1,1,1,1,1,1,1,1,1,1,1,1,1,1,1,1,1,1,1,1,1,1,1,1,1,1,1,1,1,1,1,
1,1,1,1,1,1,1,1,1,1,1,1,1,1,1,1,1,1,1,4),(0.,0.0329955678841871),(8.30203615430837,
9.30077714598354,10.2995181376587,11.2982591293339,12.2970001210091,13.2957411126842,
14.2944821043594,15.2932230960346,16.2919640877097,17.2907050793849,18.2894460710601,
19.2881870627352,20.2869280544104,21.2856690460856,22.2844100377608,23.2831510294359,
24.2818920211111,25.2806330127863,26.2793740044614,27.2781149961366,28.2768559878118,
29.2755969794869,30.2743379711621,31.2730789628373,32.2718199545125,33.2705609461876,
34.2693019378628,35.268042929538,36.2667839212131,37.2655249128883,38.2642659045635,
39.2630068962386,40.2617478879138,41.260488879589,42.2592298712642,43.2579708629393,
44.2567118546145,45.2554528462897,46.2541938379648,47.25293482964,48.2516758213152,
49.2504168129903,50.2491578046655,51.2478987963407,52.2466397880159,53.245380779691,
54.2441217713662,55.2428627630414,56.2416037547165,57.2403447463917,58.2390857380669,
59.237826729742,60.2365677214172,61.2353087130924,62.2340497047676,63.2327906964427,
64.2315316881179),.UNSPECIFIED.);
#1640=FACE_OUTER_BOUND('',#2744,.T.);
#1641=FACE_OUTER_BOUND('',#2745,.T.);
#1642=FACE_OUTER_BOUND('',#2746,.T.);
#1643=FACE_OUTER_BOUND('',#2747,.T.);
#1644=FACE_OUTER_BOUND('',#2748,.T.);
#1645=FACE_OUTER_BOUND('',#2749,.T.);
#1646=FACE_OUTER_BOUND('',#2750,.T.);
#1647=FACE_OUTER_BOUND('',#2751,.T.);
#1648=FACE_OUTER_BOUND('',#2752,.T.);
#1649=FACE_OUTER_BOUND('',#2753,.T.);
#1650=FACE_OUTER_BOUND('',#2754,.T.);
#1651=FACE_OUTER_BOUND('',#2755,.T.);
#1652=FACE_OUTER_BOUND('',#2756,.T.);
#1653=FACE_OUTER_BOUND('',#2757,.T.);
#1654=FACE_OUTER_BOUND('',#2758,.T.);
#1655=FACE_OUTER_BOUND('',#2759,.T.);
#1656=FACE_OUTER_BOUND('',#2760,.T.);
#1657=FACE_OUTER_BOUND('',#2761,.T.);
#1658=FACE_OUTER_BOUND('',#2762,.T.);
#1659=FACE_OUTER_BOUND('',#2763,.T.);
#1660=FACE_OUTER_BOUND('',#2764,.T.);
#1661=FACE_OUTER_BOUND('',#2765,.T.);
#1662=FACE_OUTER_BOUND('',#2766,.T.);
#1663=FACE_OUTER_BOUND('',#2767,.T.);
#1664=FACE_OUTER_BOUND('',#2768,.T.);
#1665=FACE_OUTER_BOUND('',#2769,.T.);
#1666=FACE_OUTER_BOUND('',#2770,.T.);
#1667=FACE_OUTER_BOUND('',#2771,.T.);
#1668=FACE_OUTER_BOUND('',#2772,.T.);
#1669=FACE_OUTER_BOUND('',#2773,.T.);
#1670=FACE_OUTER_BOUND('',#2775,.T.);
#1671=FACE_OUTER_BOUND('',#2776,.T.);
#2744=EDGE_LOOP('',(#16362,#16363,#16364,#16365));
#2745=EDGE_LOOP('',(#16366,#16367,#16368,#16369));
#2746=EDGE_LOOP('',(#16370,#16371,#16372,#16373));
#2747=EDGE_LOOP('',(#16374,#16375,#16376,#16377));
#2748=EDGE_LOOP('',(#16378,#16379,#16380,#16381));
#2749=EDGE_LOOP('',(#16382,#16383,#16384,#16385));
#2750=EDGE_LOOP('',(#16386,#16387,#16388,#16389));
#2751=EDGE_LOOP('',(#16390,#16391,#16392,#16393));
#2752=EDGE_LOOP('',(#16394,#16395,#16396,#16397));
#2753=EDGE_LOOP('',(#16398,#16399,#16400,#16401));
#2754=EDGE_LOOP('',(#16402,#16403,#16404,#16405));
#2755=EDGE_LOOP('',(#16406,#16407,#16408,#16409));
#2756=EDGE_LOOP('',(#16410,#16411,#16412,#16413));
#2757=EDGE_LOOP('',(#16414,#16415,#16416,#16417));
#2758=EDGE_LOOP('',(#16418,#16419,#16420,#16421));
#2759=EDGE_LOOP('',(#16422,#16423,#16424,#16425));
#2760=EDGE_LOOP('',(#16426,#16427,#16428,#16429,#16430,#16431,#16432,#16433));
#2761=EDGE_LOOP('',(#16434,#16435,#16436,#16437,#16438,#16439,#16440,#16441,
#16442,#16443,#16444,#16445,#16446,#16447,#16448,#16449,#16450,#16451,#16452,
#16453));
#2762=EDGE_LOOP('',(#16454,#16455,#16456,#16457));
#2763=EDGE_LOOP('',(#16458,#16459,#16460,#16461));
#2764=EDGE_LOOP('',(#16462,#16463,#16464,#16465));
#2765=EDGE_LOOP('',(#16466,#16467,#16468,#16469));
#2766=EDGE_LOOP('',(#16470,#16471,#16472,#16473));
#2767=EDGE_LOOP('',(#16474,#16475,#16476,#16477));
#2768=EDGE_LOOP('',(#16478,#16479,#16480,#16481));
#2769=EDGE_LOOP('',(#16482,#16483,#16484,#16485,#16486,#16487));
#2770=EDGE_LOOP('',(#16488,#16489,#16490,#16491,#16492,#16493,#16494,#16495,
#16496,#16497,#16498,#16499,#16500,#16501,#16502,#16503,#16504,#16505,#16506,
#16507,#16508));
#2771=EDGE_LOOP('',(#16509,#16510,#16511,#16512,#16513));
#2772=EDGE_LOOP('',(#16514,#16515,#16516,#16517));
#2773=EDGE_LOOP('',(#16518));
#2774=EDGE_LOOP('',(#16519,#16520,#16521,#16522,#16523,#16524));
#2775=EDGE_LOOP('',(#16525,#16526,#16527,#16528,#16529,#16530));
#2776=EDGE_LOOP('',(#16531));
#3105=CIRCLE('',#19703,1.4635);
#3106=CIRCLE('',#19712,1.17775);
#3107=CIRCLE('',#19721,1.4635);
#3108=CIRCLE('',#19722,0.999999999999998);
#3109=CIRCLE('',#19724,1.17775);
#3110=CIRCLE('',#19733,1.4635);
#3111=CIRCLE('',#19734,1.4635);
#3112=CIRCLE('',#19737,3.);
#4589=B_SPLINE_CURVE_WITH_KNOTS('',3,(#97847,#97848,#97849,#97850,#97851,
#97852,#97853,#97854,#97855,#97856),.UNSPECIFIED.,.F.,.F.,(4,3,3,4),(-4.09202352044853,
-3.98935724892517,-2.99201793669388,-2.07317267331972),.UNSPECIFIED.);
#4590=B_SPLINE_CURVE_WITH_KNOTS('',3,(#97859,#97860,#97861,#97862,#97863,
#97864,#97865),.UNSPECIFIED.,.F.,.F.,(4,3,4),(0.,0.998740991675169,1.12274180646096),
 .UNSPECIFIED.);
#4591=B_SPLINE_CURVE_WITH_KNOTS('',3,(#97870,#97871,#97872,#97873,#97874,
#97875,#97876,#97877,#97878,#97879,#97880,#97881,#97882,#97883,#97884,#97885,
#97886,#97887,#97888,#97889,#97890,#97891),.UNSPECIFIED.,.F.,.F.,(4,3,3,
3,3,3,3,4),(-10.3752088276281,-9.97339312231293,-8.97605381008164,-7.97871449785035,
-6.98137518561906,-5.98403587338776,-4.98669656115647,-4.09202352044853),
 .UNSPECIFIED.);
#4592=B_SPLINE_CURVE_WITH_KNOTS('',3,(#97892,#97893,#97894,#97895,#97896,
#97897,#97898,#97899,#97900,#97901,#97902,#97903,#97904,#97905,#97906,#97907,
#97908,#97909,#97910,#97911,#97912,#97913),.UNSPECIFIED.,.F.,.F.,(4,3,3,
3,3,3,3,4),(1.12274180646096,1.99748198335034,2.99622297502551,3.99496396670068,
4.99370495837585,5.99244595005102,6.99118694172619,7.40592711364054),
 .UNSPECIFIED.);
#4593=B_SPLINE_CURVE_WITH_KNOTS('',3,(#97918,#97919,#97920,#97921,#97922,
#97923,#97924,#97925,#97926,#97927,#97928,#97929,#97930,#97931,#97932,#97933,
#97934,#97935,#97936,#97937,#97938,#97939),.UNSPECIFIED.,.F.,.F.,(4,3,3,
3,3,3,3,4),(-16.6583941348077,-15.9574289957007,-14.9600896834694,-13.9627503712381,
-12.9654110590068,-11.9680717467755,-10.9707324345442,-10.3752088276281),
 .UNSPECIFIED.);
#4594=B_SPLINE_CURVE_WITH_KNOTS('',3,(#97940,#97941,#97942,#97943,#97944,
#97945,#97946,#97947,#97948,#97949,#97950,#97951,#97952,#97953,#97954,#97955,
#97956,#97957,#97958,#97959,#97960,#97961),.UNSPECIFIED.,.F.,.F.,(4,3,3,
3,3,3,3,4),(7.40592711364054,7.98992793340136,8.98866892507653,9.9874099167517,
10.9861509084269,11.984891900102,12.9836328917772,13.6891124208201),
 .UNSPECIFIED.);
#4595=B_SPLINE_CURVE_WITH_KNOTS('',3,(#97966,#97967,#97968,#97969,#97970,
#97971,#97972,#97973,#97974,#97975,#97976,#97977,#97978,#97979,#97980,#97981,
#97982,#97983,#97984,#97985,#97986,#97987),.UNSPECIFIED.,.F.,.F.,(4,3,3,
3,3,3,3,4),(-22.9415794419873,-21.9414648690884,-20.9441255568571,-19.9467862446259,
-18.9494469323946,-17.9521076201633,-16.954768307932,-16.6583941348077),
 .UNSPECIFIED.);
#4596=B_SPLINE_CURVE_WITH_KNOTS('',3,(#97988,#97989,#97990,#97991,#97992,
#97993,#97994,#97995,#97996,#97997,#97998,#97999,#98000,#98001,#98002,#98003,
#98004,#98005,#98006,#98007,#98008,#98009),.UNSPECIFIED.,.F.,.F.,(4,3,3,
3,3,3,3,4),(13.6891124208201,13.9823738834524,14.9811148751276,15.9798558668027,
16.9785968584779,17.9773378501531,18.9760788418282,19.9722977279997),
 .UNSPECIFIED.);
#4597=B_SPLINE_CURVE_WITH_KNOTS('',3,(#98014,#98015,#98016,#98017,#98018,
#98019,#98020,#98021,#98022,#98023,#98024,#98025,#98026,#98027,#98028,#98029,
#98030,#98031,#98032,#98033,#98034,#98035),.UNSPECIFIED.,.F.,.F.,(4,3,3,
3,3,3,3,4),(-29.2247647491669,-28.9228400547075,-27.9255007424762,-26.9281614302449,
-25.9308221180136,-24.9334828057823,-23.936143493551,-22.9415794419873),
 .UNSPECIFIED.);
#4598=B_SPLINE_CURVE_WITH_KNOTS('',3,(#98036,#98037,#98038,#98039,#98040,
#98041,#98042,#98043,#98044,#98045,#98046,#98047,#98048,#98049,#98050,#98051,
#98052,#98053,#98054,#98055,#98056,#98057),.UNSPECIFIED.,.F.,.F.,(4,3,3,
3,3,3,3,4),(19.9722977279997,20.9735608251786,21.9723018168537,22.9710428085289,
23.9697838002041,24.9685247918793,25.9672657835544,26.2554830351793),
 .UNSPECIFIED.);
#4599=B_SPLINE_CURVE_WITH_KNOTS('',3,(#98062,#98063,#98064,#98065,#98066,
#98067,#98068,#98069,#98070,#98071,#98072,#98073,#98074,#98075,#98076,#98077,
#98078,#98079,#98080,#98081,#98082,#98083),.UNSPECIFIED.,.F.,.F.,(4,3,3,
3,3,3,3,4),(-35.5079500563465,-34.9068759280953,-33.909536615864,-32.9121973036327,
-31.9148579914014,-30.9175186791701,-29.9201793669388,-29.2247647491669),
 .UNSPECIFIED.);
#4600=B_SPLINE_CURVE_WITH_KNOTS('',3,(#98084,#98085,#98086,#98087,#98088,
#98089,#98090,#98091,#98092,#98093,#98094,#98095,#98096,#98097,#98098,#98099,
#98100,#98101,#98102,#98103,#98104,#98105),.UNSPECIFIED.,.F.,.F.,(4,3,3,
3,3,3,3,4),(26.2554830351793,26.9660067752296,27.9647477669048,28.9634887585799,
29.9622297502551,30.9609707419303,31.9597117336054,32.5386683423589),
 .UNSPECIFIED.);
#4601=B_SPLINE_CURVE_WITH_KNOTS('',3,(#98110,#98111,#98112,#98113,#98114,
#98115,#98116,#98117,#98118,#98119,#98120,#98121,#98122,#98123,#98124,#98125,
#98126,#98127,#98128,#98129,#98130,#98131),.UNSPECIFIED.,.F.,.F.,(4,3,3,
3,3,3,3,4),(-41.791135363526,-40.890911801483,-39.8935724892517,-38.8962331770204,
-37.8988938647891,-36.9015545525578,-35.9042152403266,-35.5079500563465),
 .UNSPECIFIED.);
#4602=B_SPLINE_CURVE_WITH_KNOTS('',3,(#98132,#98133,#98134,#98135,#98136,
#98137,#98138,#98139,#98140,#98141,#98142,#98143,#98144,#98145,#98146,#98147,
#98148,#98149,#98150,#98151,#98152,#98153),.UNSPECIFIED.,.F.,.F.,(4,3,3,
3,3,3,3,4),(32.5386683423589,32.9584527252806,33.9571937169558,34.955934708631,
35.9546757003061,36.9534166919813,37.9521576836565,38.8218536495385),
 .UNSPECIFIED.);
#4603=B_SPLINE_CURVE_WITH_KNOTS('',3,(#98158,#98159,#98160,#98161,#98162,
#98163,#98164,#98165,#98166,#98167,#98168,#98169,#98170,#98171,#98172,#98173,
#98174,#98175,#98176,#98177,#98178,#98179,#98180,#98181,#98182),
 .UNSPECIFIED.,.F.,.F.,(4,3,3,3,3,3,3,3,4),(-48.0743206707056,-47.8722869871021,
-46.8749476748708,-45.8776083626395,-44.8802690504082,-43.8829297381769,
-42.8855904259456,-41.8882511137143,-41.791135363526),.UNSPECIFIED.);
#4604=B_SPLINE_CURVE_WITH_KNOTS('',3,(#98183,#98184,#98185,#98186,#98187,
#98188,#98189,#98190,#98191,#98192,#98193,#98194,#98195,#98196,#98197,#98198,
#98199,#98200,#98201,#98202,#98203,#98204,#98205,#98206,#98207),
 .UNSPECIFIED.,.F.,.F.,(4,3,3,3,3,3,3,3,4),(38.8218536495385,38.9508986753316,
39.9496396670068,40.948380658682,41.9471216503571,42.9458626420323,43.9446036337075,
44.9433446253827,45.1050389567181),.UNSPECIFIED.);
#4605=B_SPLINE_CURVE_WITH_KNOTS('',3,(#98213,#98214,#98215,#98216,#98217,
#98218,#98219,#98220,#98221),.UNSPECIFIED.,.F.,.F.,(4,1,1,1,1,1,4),(59.6902604182061,
60.4855660468338,61.4829053590651,62.4802446712963,63.4775839835276,64.4749232957589,
65.4722626079902),.UNSPECIFIED.);
#4606=B_SPLINE_CURVE_WITH_KNOTS('',3,(#98224,#98225,#98226,#98227,#98228,
#98229,#98230,#98231),.UNSPECIFIED.,.F.,.F.,(4,1,1,1,1,4),(59.6902604182061,
60.2365677214172,61.2353087130924,62.2340497047676,63.2327906964427,64.2315316881179),
 .UNSPECIFIED.);
#4607=B_SPLINE_CURVE_WITH_KNOTS('',3,(#98236,#98237,#98238,#98239,#98240,
#98241,#98242,#98243,#98244,#98245,#98246),.UNSPECIFIED.,.F.,.F.,(4,1,1,
1,1,1,1,1,4),(53.4070751110265,53.5041908612147,54.501530173446,55.4988694856773,
56.4962087979086,57.4935481101399,58.4908874223712,59.4882267346025,59.6902604182061),
 .UNSPECIFIED.);
#4608=B_SPLINE_CURVE_WITH_KNOTS('',3,(#98247,#98248,#98249,#98250,#98251,
#98252,#98253,#98254,#98255,#98256),.UNSPECIFIED.,.F.,.F.,(4,1,1,1,1,1,
1,4),(53.4070751110265,54.2441217713662,55.2428627630414,56.2416037547165,
57.2403447463917,58.2390857380669,59.237826729742,59.6902604182061),
 .UNSPECIFIED.);
#4609=B_SPLINE_CURVE_WITH_KNOTS('',3,(#98261,#98262,#98263,#98264,#98265,
#98266,#98267,#98268,#98269,#98270),.UNSPECIFIED.,.F.,.F.,(4,1,1,1,1,1,
1,4),(47.1238898038469,47.520154987827,48.5174943000582,49.5148336122895,
50.5121729245208,51.5095122367521,52.5068515489834,53.4070751110265),
 .UNSPECIFIED.);
#4610=B_SPLINE_CURVE_WITH_KNOTS('',3,(#98271,#98272,#98273,#98274,#98275,
#98276,#98277,#98278,#98279,#98280,#98281),.UNSPECIFIED.,.F.,.F.,(4,1,1,
1,1,1,1,1,4),(47.1238898038469,47.25293482964,48.2516758213152,49.2504168129903,
50.2491578046655,51.2478987963407,52.2466397880159,53.245380779691,53.4070751110265),
 .UNSPECIFIED.);
#4611=B_SPLINE_CURVE_WITH_KNOTS('',3,(#98286,#98287,#98288,#98289,#98290,
#98291,#98292,#98293,#98294,#98295),.UNSPECIFIED.,.F.,.F.,(4,1,1,1,1,1,
1,4),(40.8407044966673,41.5361191144392,42.5334584266705,43.5307977389018,
44.5281370511331,45.5254763633644,46.5228156755957,47.1238898038469),
 .UNSPECIFIED.);
#4612=B_SPLINE_CURVE_WITH_KNOTS('',3,(#98296,#98297,#98298,#98299,#98300,
#98301,#98302,#98303,#98304,#98305),.UNSPECIFIED.,.F.,.F.,(4,1,1,1,1,1,
1,4),(40.8407044966673,41.260488879589,42.2592298712642,43.2579708629393,
44.2567118546145,45.2554528462897,46.2541938379648,47.1238898038469),
 .UNSPECIFIED.);
#4613=B_SPLINE_CURVE_WITH_KNOTS('',3,(#98310,#98311,#98312,#98313,#98314,
#98315,#98316,#98317,#98318,#98319),.UNSPECIFIED.,.F.,.F.,(4,1,1,1,1,1,
1,4),(34.5575191894877,35.5520832410514,36.5494225532827,37.546761865514,
38.5441011777453,39.5414404899766,40.5387798022079,40.8407044966673),
 .UNSPECIFIED.);
#4614=B_SPLINE_CURVE_WITH_KNOTS('',3,(#98320,#98321,#98322,#98323,#98324,
#98325,#98326,#98327,#98328,#98329),.UNSPECIFIED.,.F.,.F.,(4,1,1,1,1,1,
1,4),(34.5575191894877,35.268042929538,36.2667839212131,37.2655249128883,
38.2642659045635,39.2630068962386,40.2617478879138,40.8407044966673),
 .UNSPECIFIED.);
#4615=B_SPLINE_CURVE_WITH_KNOTS('',3,(#98334,#98335,#98336,#98337,#98338,
#98339,#98340,#98341,#98342,#98343,#98344),.UNSPECIFIED.,.F.,.F.,(4,1,1,
1,1,1,1,1,4),(28.2743338823081,28.5707080554324,29.5680473676637,30.565386679895,
31.5627259921263,32.5600653043576,33.5574046165888,34.5547439288201,34.5575191894877),
 .UNSPECIFIED.);
#4616=B_SPLINE_CURVE_WITH_KNOTS('',3,(#98345,#98346,#98347,#98348,#98349,
#98350,#98351,#98352,#98353,#98354,#98355),.UNSPECIFIED.,.F.,.F.,(4,1,1,
1,1,1,1,1,4),(28.2743338823081,28.2768559878118,29.2755969794869,30.2743379711621,
31.2730789628373,32.2718199545125,33.2705609461876,34.2693019378628,34.5575191894877),
 .UNSPECIFIED.);
#4617=B_SPLINE_CURVE_WITH_KNOTS('',3,(#98360,#98361,#98362,#98363,#98364,
#98365,#98366,#98367,#98368,#98369),.UNSPECIFIED.,.F.,.F.,(4,1,1,1,1,1,
1,4),(21.9911485751285,22.5866721820446,23.5840114942759,24.5813508065072,
25.5786901187385,26.5760294309698,27.5733687432011,28.2743338823081),
 .UNSPECIFIED.);
#4618=B_SPLINE_CURVE_WITH_KNOTS('',3,(#98370,#98371,#98372,#98373,#98374,
#98375,#98376,#98377,#98378,#98379),.UNSPECIFIED.,.F.,.F.,(4,1,1,1,1,1,
1,4),(21.9911485751285,22.2844100377608,23.2831510294359,24.2818920211111,
25.2806330127863,26.2793740044614,27.2781149961366,28.2743338823081),
 .UNSPECIFIED.);
#4619=B_SPLINE_CURVE_WITH_KNOTS('',3,(#98384,#98385,#98386,#98387,#98388,
#98389,#98390,#98391,#98392,#98393),.UNSPECIFIED.,.F.,.F.,(4,1,1,1,1,1,
1,4),(15.7079632679489,16.6026363086569,17.5999756208882,18.5973149331195,
19.5946542453507,20.591993557582,21.5893328698133,21.9911485751285),
 .UNSPECIFIED.);
#4620=B_SPLINE_CURVE_WITH_KNOTS('',3,(#98394,#98395,#98396,#98397,#98398,
#98399,#98400,#98401,#98402,#98403),.UNSPECIFIED.,.F.,.F.,(4,1,1,1,1,1,
1,4),(15.7079632679489,16.2919640877097,17.2907050793849,18.2894460710601,
19.2881870627352,20.2869280544104,21.2856690460856,21.9911485751285),
 .UNSPECIFIED.);
#4621=B_SPLINE_CURVE_WITH_KNOTS('',3,(#98406,#98407,#98408,#98409,#98410,
#98411,#98412,#98413,#98414,#98415,#98416,#98417,#98418,#98419,#98420,#98421,
#98422,#98423,#98424,#98425,#98426,#98427,#98428,#98429,#98430,#98431,#98432,
#98433,#98434,#98435,#98436,#98437,#98438,#98439,#98440,#98441,#98442,#98443,
#98444,#98445,#98446,#98447,#98448,#98449,#98450,#98451,#98452,#98453,#98454,
#98455,#98456,#98457,#98458,#98459,#98460,#98461,#98462,#98463,#98464,#98465,
#98466,#98467,#98468,#98469,#98470,#98471,#98472,#98473,#98474,#98475,#98476,
#98477,#98478,#98479,#98480,#98481,#98482,#98483,#98484,#98485,#98486,#98487,
#98488,#98489,#98490,#98491,#98492,#98493,#98494,#98495,#98496,#98497,#98498,
#98499,#98500,#98501,#98502,#98503,#98504,#98505,#98506,#98507,#98508,#98509,
#98510,#98511,#98512,#98513,#98514,#98515,#98516,#98517,#98518,#98519,#98520,
#98521,#98522,#98523,#98524,#98525,#98526,#98527,#98528,#98529,#98530,#98531,
#98532,#98533,#98534,#98535,#98536,#98537,#98538,#98539,#98540,#98541,#98542,
#98543,#98544,#98545,#98546,#98547,#98548,#98549,#98550,#98551,#98552,#98553,
#98554,#98555,#98556,#98557,#98558,#98559,#98560,#98561,#98562,#98563,#98564,
#98565,#98566,#98567,#98568,#98569,#98570,#98571,#98572,#98573,#98574,#98575,
#98576,#98577,#98578,#98579,#98580,#98581,#98582,#98583,#98584,#98585,#98586,
#98587,#98588,#98589),.UNSPECIFIED.,.F.,.F.,(4,3,3,3,3,3,3,3,3,3,3,3,3,
3,3,3,3,3,3,3,3,3,3,3,3,3,3,3,3,3,3,3,3,3,3,3,3,3,3,3,3,3,3,3,3,3,3,3,3,
3,3,3,3,3,3,3,3,3,3,3,3,4),(-0.753008129282157,-0.73786527623977,-0.724615279827681,
-0.717098895378918,-0.713787159730779,-0.698410405843186,-0.682933186955955,
-0.679855182994275,-0.664200486121929,-0.648032895532493,-0.639949100237776,
-0.635216460798448,-0.632188335448626,-0.631865304943058,-0.61690168950646,
-0.601227264223793,-0.589281754696583,-0.585169909644513,-0.581926626388212,
-0.566053286590164,-0.550081089144897,-0.538976613860202,-0.534874931105234,
-0.531662796183257,-0.515550254278411,-0.505663188006116,-0.489273050645826,
-0.485270605061208,-0.482408633379521,-0.466387560157893,-0.450041076803483,
-0.440603703343523,-0.433818542109577,-0.430853819905116,-0.414279731357498,
-0.397826739572435,-0.386184414348117,-0.382110700287907,-0.379222591070396,
-0.3745420891238,-0.358536027981697,-0.343522511777778,-0.33597373730796,
-0.331449848714152,-0.327650568312031,-0.31091799154362,-0.293972525585514,
-0.280086368776722,-0.276804967864447,-0.27376471063138,-0.256096304490863,
-0.239324632856325,-0.238427898350346,-0.228865409785226,-0.224320857142883,
-0.220678125153778,-0.203840509088529,-0.186665330500045,-0.174296660164717,
-0.169386715434793,-0.1662786999892,-0.161927989829389),.UNSPECIFIED.);
#4622=B_SPLINE_CURVE_WITH_KNOTS('',3,(#98591,#98592,#98593,#98594,#98595,
#98596,#98597,#98598,#98599,#98600,#98601,#98602,#98603,#98604,#98605,#98606,
#98607,#98608,#98609,#98610,#98611,#98612,#98613,#98614,#98615,#98616,#98617,
#98618,#98619,#98620,#98621,#98622,#98623,#98624,#98625,#98626,#98627,#98628,
#98629,#98630,#98631,#98632,#98633,#98634,#98635,#98636,#98637,#98638,#98639,
#98640,#98641,#98642,#98643,#98644,#98645,#98646,#98647,#98648,#98649,#98650,
#98651),.UNSPECIFIED.,.F.,.F.,(4,3,3,3,3,3,3,3,3,3,3,3,3,3,3,3,3,3,3,3,
4),(-0.204609524178332,-0.187229444739388,-0.170308057115437,-0.160178775707448,
-0.152889242910402,-0.149873358866868,-0.133572111564231,-0.129790931483479,
-0.113567065048044,-0.105824638338513,-0.0991132485902469,-0.0961971109838234,
-0.0801003606559814,-0.0641272763676895,-0.0555369672079658,-0.0490619748994989,
-0.0460483768969834,-0.0308260628889665,-0.0154130314444832,-0.000938554365243004,
0.),.UNSPECIFIED.);
#4623=B_SPLINE_CURVE_WITH_KNOTS('',3,(#98654,#98655,#98656,#98657,#98658,
#98659,#98660,#98661,#98662,#98663,#98664,#98665,#98666,#98667,#98668,#98669,
#98670,#98671,#98672,#98673,#98674,#98675,#98676,#98677,#98678,#98679,#98680,
#98681,#98682,#98683,#98684,#98685,#98686,#98687,#98688,#98689,#98690,#98691,
#98692,#98693),.UNSPECIFIED.,.F.,.F.,(4,3,3,3,3,3,3,3,3,3,3,3,3,4),(-0.161927989829389,
-0.14445211284144,-0.127148387454473,-0.119019661086295,-0.114739079705313,
-0.110791737995318,-0.0974340408014069,-0.0803127274975295,-0.0628060442148566,
-0.0579606305293774,-0.0547831112214332,-0.0372028960526897,-0.0186014480263448,
0.),.UNSPECIFIED.);
#4624=B_SPLINE_CURVE_WITH_KNOTS('',3,(#98926,#98927,#98928,#98929,#98930,
#98931,#98932,#98933),.UNSPECIFIED.,.F.,.F.,(4,1,1,1,1,4),(11.6159397475004,
12.6132790597317,13.610618371963,14.6079576841943,15.6052969964256,15.7079632679489),
 .UNSPECIFIED.);
#4625=B_SPLINE_CURVE_WITH_KNOTS('',3,(#98934,#98935,#98936,#98937,#98938,
#98939,#98940,#98941,#98942,#98943,#98944,#98945,#98946,#98947,#98948,#98949,
#98950,#98951,#98952,#98953,#98954,#98955,#98956,#98957,#98958,#98959,#98960,
#98961,#98962,#98963,#98964,#98965,#98966,#98967,#98968,#98969,#98970,#98971,
#98972,#98973,#98974,#98975,#98976,#98977,#98978,#98979,#98980,#98981,#98982,
#98983,#98984,#98985,#98986,#98987,#98988,#98989,#98990,#98991,#98992,#98993,
#98994,#98995,#98996,#98997,#98998,#98999,#99000,#99001,#99002,#99003,#99004,
#99005,#99006,#99007,#99008,#99009,#99010,#99011,#99012,#99013,#99014,#99015),
 .UNSPECIFIED.,.F.,.F.,(4,3,3,3,3,3,3,3,3,3,3,3,3,3,3,3,3,3,3,3,3,3,3,3,
3,3,3,4),(-0.275362278356883,-0.263900331993925,-0.246578497995159,-0.237038384704303,
-0.233158136947895,-0.215956509362073,-0.204627653192289,-0.199386939936824,
-0.195964342542413,-0.179215296048088,-0.162902384492512,-0.153508203370335,
-0.148362000491666,-0.144152894533275,-0.128300920501684,-0.125325660003802,
-0.108643799301575,-0.101041482676622,-0.0956984034813221,-0.0926133309948634,
-0.0768446933414484,-0.0611549478274358,-0.0532963163041718,-0.0475064809797105,
-0.0447082261449061,-0.0296004251347768,-0.0148002125673884,0.),
 .UNSPECIFIED.);
#4626=B_SPLINE_CURVE_WITH_KNOTS('',3,(#99016,#99017,#99018,#99019,#99020,
#99021,#99022,#99023,#99024,#99025,#99026,#99027,#99028,#99029,#99030,#99031),
 .UNSPECIFIED.,.F.,.F.,(4,3,3,3,3,4),(-52.3386551307564,-51.8616442360272,
-50.8643049237959,-49.8669656115647,-48.8696262993334,-48.0743206707056),
 .UNSPECIFIED.);
#4627=B_SPLINE_CURVE_WITH_KNOTS('',3,(#99034,#99035,#99036,#99037,#99038,
#99039,#99040,#99041,#99042),.UNSPECIFIED.,.F.,.F.,(4,1,1,1,1,1,4),(10.3752088276281,
11.2982591293339,12.2970001210091,13.2957411126842,14.2944821043594,15.2932230960346,
15.7079632679489),.UNSPECIFIED.);
#4628=B_SPLINE_CURVE_WITH_KNOTS('',3,(#99317,#99318,#99319,#99320,#99321,
#99322,#99323,#99324,#99325,#99326,#99327,#99328,#99329,#99330,#99331,#99332,
#99333,#99334,#99335),.UNSPECIFIED.,.F.,.F.,(4,3,3,3,3,3,4),(45.1050389567181,
45.9420856170578,46.940826608733,47.9395676004082,48.9383085920833,49.9370495837585,
50.2654824574366),.UNSPECIFIED.);
#4629=B_SPLINE_CURVE_WITH_KNOTS('',3,(#99336,#99337,#99338,#99339,#99340,
#99341,#99342,#99343,#99344,#99345,#99346,#99347,#99348,#99349,#99350,#99351,
#99352,#99353,#99354,#99355,#99356,#99357,#99358,#99359,#99360,#99361,#99362,
#99363,#99364,#99365,#99366,#99367,#99368,#99369,#99370,#99371,#99372,#99373,
#99374,#99375,#99376,#99377,#99378,#99379,#99380,#99381,#99382,#99383,#99384,
#99385,#99386,#99387,#99388,#99389,#99390,#99391,#99392,#99393,#99394,#99395,
#99396,#99397,#99398,#99399,#99400,#99401,#99402,#99403,#99404,#99405,#99406,
#99407,#99408,#99409,#99410,#99411,#99412,#99413,#99414,#99415,#99416,#99417,
#99418,#99419,#99420),.UNSPECIFIED.,.F.,.F.,(4,3,3,3,3,3,3,3,3,3,3,3,3,
3,3,3,3,3,3,3,3,3,3,3,3,3,3,3,4),(-0.276631791712721,-0.267572232012667,
-0.252957312390642,-0.247122920332528,-0.24209048560573,-0.22681681001417,
-0.216036201245221,-0.21183998522367,-0.208623843551383,-0.192852303440504,
-0.176802879296701,-0.16774514443817,-0.162460607960523,-0.15957229971733,
-0.143044531332662,-0.140571939862575,-0.124627165055967,-0.116201869211177,
-0.111145681876705,-0.108000260957167,-0.0914514087508209,-0.0745399955216332,
-0.0650233471421523,-0.0590680435779011,-0.0560616749739794,-0.0530529570050865,
-0.0355838889451872,-0.0177919444725936,0.),.UNSPECIFIED.);
#5498=LINE('',#97845,#6402);
#5499=LINE('',#97869,#6403);
#5500=LINE('',#97917,#6404);
#5501=LINE('',#97965,#6405);
#5502=LINE('',#98013,#6406);
#5503=LINE('',#98061,#6407);
#5504=LINE('',#98109,#6408);
#5505=LINE('',#98157,#6409);
#5506=LINE('',#98211,#6410);
#5507=LINE('',#98235,#6411);
#5508=LINE('',#98260,#6412);
#5509=LINE('',#98285,#6413);
#5510=LINE('',#98309,#6414);
#5511=LINE('',#98333,#6415);
#5512=LINE('',#98359,#6416);
#5513=LINE('',#98383,#6417);
#5514=LINE('',#98695,#6418);
#5515=LINE('',#99047,#6419);
#5516=LINE('',#99049,#6420);
#5517=LINE('',#99051,#6421);
#5518=LINE('',#99052,#6422);
#5519=LINE('',#99055,#6423);
#5520=LINE('',#99057,#6424);
#5521=LINE('',#99058,#6425);
#5522=LINE('',#99061,#6426);
#5523=LINE('',#99063,#6427);
#5524=LINE('',#99064,#6428);
#5525=LINE('',#99067,#6429);
#5526=LINE('',#99069,#6430);
#5527=LINE('',#99070,#6431);
#5528=LINE('',#99073,#6432);
#5529=LINE('',#99075,#6433);
#5530=LINE('',#99076,#6434);
#5531=LINE('',#99078,#6435);
#5532=LINE('',#99079,#6436);
#5533=LINE('',#99430,#6437);
#6402=VECTOR('',#23147,1.5);
#6403=VECTOR('',#23152,1.5);
#6404=VECTOR('',#23155,1.5);
#6405=VECTOR('',#23158,1.5);
#6406=VECTOR('',#23161,1.5);
#6407=VECTOR('',#23164,1.5);
#6408=VECTOR('',#23167,1.5);
#6409=VECTOR('',#23170,1.5);
#6410=VECTOR('',#23173,1.17775);
#6411=VECTOR('',#23178,1.17775);
#6412=VECTOR('',#23181,1.17775);
#6413=VECTOR('',#23184,1.17775);
#6414=VECTOR('',#23187,1.17775);
#6415=VECTOR('',#23190,1.17775);
#6416=VECTOR('',#23193,1.17775);
#6417=VECTOR('',#23196,1.17775);
#6418=VECTOR('',#23201,1.25);
#6419=VECTOR('',#23210,10.);
#6420=VECTOR('',#23211,10.);
#6421=VECTOR('',#23212,10.);
#6422=VECTOR('',#23213,10.);
#6423=VECTOR('',#23216,10.);
#6424=VECTOR('',#23217,10.);
#6425=VECTOR('',#23218,10.);
#6426=VECTOR('',#23221,10.);
#6427=VECTOR('',#23222,10.);
#6428=VECTOR('',#23223,10.);
#6429=VECTOR('',#23226,10.);
#6430=VECTOR('',#23227,10.);
#6431=VECTOR('',#23228,10.);
#6432=VECTOR('',#23231,10.);
#6433=VECTOR('',#23232,10.);
#6434=VECTOR('',#23233,10.);
#6435=VECTOR('',#23236,10.);
#6436=VECTOR('',#23237,10.);
#6437=VECTOR('',#23254,2.25);
#8205=VERTEX_POINT('',#97843);
#8206=VERTEX_POINT('',#97844);
#8207=VERTEX_POINT('',#97846);
#8208=VERTEX_POINT('',#97857);
#8209=VERTEX_POINT('',#97867);
#8210=VERTEX_POINT('',#97868);
#8211=VERTEX_POINT('',#97915);
#8212=VERTEX_POINT('',#97916);
#8213=VERTEX_POINT('',#97963);
#8214=VERTEX_POINT('',#97964);
#8215=VERTEX_POINT('',#98011);
#8216=VERTEX_POINT('',#98012);
#8217=VERTEX_POINT('',#98059);
#8218=VERTEX_POINT('',#98060);
#8219=VERTEX_POINT('',#98107);
#8220=VERTEX_POINT('',#98108);
#8221=VERTEX_POINT('',#98155);
#8222=VERTEX_POINT('',#98156);
#8223=VERTEX_POINT('',#98209);
#8224=VERTEX_POINT('',#98210);
#8225=VERTEX_POINT('',#98212);
#8226=VERTEX_POINT('',#98222);
#8227=VERTEX_POINT('',#98233);
#8228=VERTEX_POINT('',#98234);
#8229=VERTEX_POINT('',#98258);
#8230=VERTEX_POINT('',#98259);
#8231=VERTEX_POINT('',#98283);
#8232=VERTEX_POINT('',#98284);
#8233=VERTEX_POINT('',#98307);
#8234=VERTEX_POINT('',#98308);
#8235=VERTEX_POINT('',#98331);
#8236=VERTEX_POINT('',#98332);
#8237=VERTEX_POINT('',#98357);
#8238=VERTEX_POINT('',#98358);
#8239=VERTEX_POINT('',#98381);
#8240=VERTEX_POINT('',#98382);
#8241=VERTEX_POINT('',#98405);
#8242=VERTEX_POINT('',#98590);
#8243=VERTEX_POINT('',#98652);
#8244=VERTEX_POINT('',#98694);
#8245=VERTEX_POINT('',#98925);
#8246=VERTEX_POINT('',#99033);
#8247=VERTEX_POINT('',#99045);
#8248=VERTEX_POINT('',#99046);
#8249=VERTEX_POINT('',#99048);
#8250=VERTEX_POINT('',#99050);
#8251=VERTEX_POINT('',#99054);
#8252=VERTEX_POINT('',#99056);
#8253=VERTEX_POINT('',#99060);
#8254=VERTEX_POINT('',#99062);
#8255=VERTEX_POINT('',#99066);
#8256=VERTEX_POINT('',#99068);
#8257=VERTEX_POINT('',#99072);
#8258=VERTEX_POINT('',#99074);
#8259=VERTEX_POINT('',#99422);
#8260=VERTEX_POINT('',#99427);
#10933=EDGE_CURVE('',#8205,#8206,#5498,.T.);
#10934=EDGE_CURVE('',#8205,#8207,#4589,.T.);
#10935=EDGE_CURVE('',#8207,#8208,#3105,.F.);
#10936=EDGE_CURVE('',#8208,#8206,#4590,.T.);
#10937=EDGE_CURVE('',#8209,#8210,#5499,.T.);
#10938=EDGE_CURVE('',#8209,#8205,#4591,.T.);
#10939=EDGE_CURVE('',#8206,#8210,#4592,.T.);
#10940=EDGE_CURVE('',#8211,#8212,#5500,.T.);
#10941=EDGE_CURVE('',#8211,#8209,#4593,.T.);
#10942=EDGE_CURVE('',#8210,#8212,#4594,.T.);
#10943=EDGE_CURVE('',#8213,#8214,#5501,.T.);
#10944=EDGE_CURVE('',#8213,#8211,#4595,.T.);
#10945=EDGE_CURVE('',#8212,#8214,#4596,.T.);
#10946=EDGE_CURVE('',#8215,#8216,#5502,.T.);
#10947=EDGE_CURVE('',#8215,#8213,#4597,.T.);
#10948=EDGE_CURVE('',#8214,#8216,#4598,.T.);
#10949=EDGE_CURVE('',#8217,#8218,#5503,.T.);
#10950=EDGE_CURVE('',#8217,#8215,#4599,.T.);
#10951=EDGE_CURVE('',#8216,#8218,#4600,.T.);
#10952=EDGE_CURVE('',#8219,#8220,#5504,.T.);
#10953=EDGE_CURVE('',#8219,#8217,#4601,.T.);
#10954=EDGE_CURVE('',#8218,#8220,#4602,.T.);
#10955=EDGE_CURVE('',#8221,#8222,#5505,.T.);
#10956=EDGE_CURVE('',#8221,#8219,#4603,.T.);
#10957=EDGE_CURVE('',#8220,#8222,#4604,.T.);
#10958=EDGE_CURVE('',#8223,#8224,#5506,.T.);
#10959=EDGE_CURVE('',#8223,#8225,#4605,.T.);
#10960=EDGE_CURVE('',#8225,#8226,#3106,.T.);
#10961=EDGE_CURVE('',#8224,#8226,#4606,.T.);
#10962=EDGE_CURVE('',#8227,#8228,#5507,.T.);
#10963=EDGE_CURVE('',#8227,#8223,#4607,.T.);
#10964=EDGE_CURVE('',#8228,#8224,#4608,.T.);
#10965=EDGE_CURVE('',#8229,#8230,#5508,.T.);
#10966=EDGE_CURVE('',#8229,#8227,#4609,.T.);
#10967=EDGE_CURVE('',#8230,#8228,#4610,.T.);
#10968=EDGE_CURVE('',#8231,#8232,#5509,.T.);
#10969=EDGE_CURVE('',#8231,#8229,#4611,.T.);
#10970=EDGE_CURVE('',#8232,#8230,#4612,.T.);
#10971=EDGE_CURVE('',#8233,#8234,#5510,.T.);
#10972=EDGE_CURVE('',#8233,#8231,#4613,.T.);
#10973=EDGE_CURVE('',#8234,#8232,#4614,.T.);
#10974=EDGE_CURVE('',#8235,#8236,#5511,.T.);
#10975=EDGE_CURVE('',#8235,#8233,#4615,.T.);
#10976=EDGE_CURVE('',#8236,#8234,#4616,.T.);
#10977=EDGE_CURVE('',#8237,#8238,#5512,.T.);
#10978=EDGE_CURVE('',#8237,#8235,#4617,.T.);
#10979=EDGE_CURVE('',#8238,#8236,#4618,.T.);
#10980=EDGE_CURVE('',#8239,#8240,#5513,.T.);
#10981=EDGE_CURVE('',#8239,#8237,#4619,.T.);
#10982=EDGE_CURVE('',#8240,#8238,#4620,.T.);
#10983=EDGE_CURVE('',#8226,#8241,#4621,.T.);
#10984=EDGE_CURVE('',#8242,#8225,#4622,.T.);
#10985=EDGE_CURVE('',#8243,#8242,#3107,.T.);
#10986=EDGE_CURVE('',#8241,#8243,#4623,.T.);
#10987=EDGE_CURVE('',#8241,#8244,#5514,.T.);
#10988=EDGE_CURVE('',#8244,#8244,#3108,.T.);
#10989=EDGE_CURVE('',#8245,#8239,#4624,.T.);
#10990=EDGE_CURVE('',#8207,#8245,#4625,.T.);
#10991=EDGE_CURVE('',#8242,#8221,#4626,.T.);
#10992=EDGE_CURVE('',#8246,#8240,#4627,.T.);
#10993=EDGE_CURVE('',#8245,#8246,#3109,.T.);
#10994=EDGE_CURVE('',#8247,#8248,#5515,.T.);
#10995=EDGE_CURVE('',#8247,#8249,#5516,.T.);
#10996=EDGE_CURVE('',#8249,#8250,#5517,.T.);
#10997=EDGE_CURVE('',#8248,#8250,#5518,.T.);
#10998=EDGE_CURVE('',#8251,#8247,#5519,.T.);
#10999=EDGE_CURVE('',#8251,#8252,#5520,.T.);
#11000=EDGE_CURVE('',#8252,#8249,#5521,.T.);
#11001=EDGE_CURVE('',#8253,#8251,#5522,.T.);
#11002=EDGE_CURVE('',#8253,#8254,#5523,.T.);
#11003=EDGE_CURVE('',#8254,#8252,#5524,.T.);
#11004=EDGE_CURVE('',#8255,#8253,#5525,.T.);
#11005=EDGE_CURVE('',#8255,#8256,#5526,.T.);
#11006=EDGE_CURVE('',#8256,#8254,#5527,.T.);
#11007=EDGE_CURVE('',#8257,#8255,#5528,.T.);
#11008=EDGE_CURVE('',#8257,#8258,#5529,.T.);
#11009=EDGE_CURVE('',#8258,#8256,#5530,.T.);
#11010=EDGE_CURVE('',#8248,#8257,#5531,.T.);
#11011=EDGE_CURVE('',#8250,#8258,#5532,.T.);
#11012=EDGE_CURVE('',#8222,#8243,#4628,.T.);
#11013=EDGE_CURVE('',#8246,#8208,#4629,.T.);
#11014=EDGE_CURVE('',#8208,#8259,#3110,.F.);
#11015=EDGE_CURVE('',#8259,#8207,#3111,.F.);
#11016=EDGE_CURVE('',#8260,#8260,#3112,.T.);
#11017=EDGE_CURVE('',#8259,#8260,#5533,.T.);
#16362=ORIENTED_EDGE('',*,*,#10933,.F.);
#16363=ORIENTED_EDGE('',*,*,#10934,.T.);
#16364=ORIENTED_EDGE('',*,*,#10935,.T.);
#16365=ORIENTED_EDGE('',*,*,#10936,.T.);
#16366=ORIENTED_EDGE('',*,*,#10937,.F.);
#16367=ORIENTED_EDGE('',*,*,#10938,.T.);
#16368=ORIENTED_EDGE('',*,*,#10933,.T.);
#16369=ORIENTED_EDGE('',*,*,#10939,.T.);
#16370=ORIENTED_EDGE('',*,*,#10940,.F.);
#16371=ORIENTED_EDGE('',*,*,#10941,.T.);
#16372=ORIENTED_EDGE('',*,*,#10937,.T.);
#16373=ORIENTED_EDGE('',*,*,#10942,.T.);
#16374=ORIENTED_EDGE('',*,*,#10943,.F.);
#16375=ORIENTED_EDGE('',*,*,#10944,.T.);
#16376=ORIENTED_EDGE('',*,*,#10940,.T.);
#16377=ORIENTED_EDGE('',*,*,#10945,.T.);
#16378=ORIENTED_EDGE('',*,*,#10946,.F.);
#16379=ORIENTED_EDGE('',*,*,#10947,.T.);
#16380=ORIENTED_EDGE('',*,*,#10943,.T.);
#16381=ORIENTED_EDGE('',*,*,#10948,.T.);
#16382=ORIENTED_EDGE('',*,*,#10949,.F.);
#16383=ORIENTED_EDGE('',*,*,#10950,.T.);
#16384=ORIENTED_EDGE('',*,*,#10946,.T.);
#16385=ORIENTED_EDGE('',*,*,#10951,.T.);
#16386=ORIENTED_EDGE('',*,*,#10952,.F.);
#16387=ORIENTED_EDGE('',*,*,#10953,.T.);
#16388=ORIENTED_EDGE('',*,*,#10949,.T.);
#16389=ORIENTED_EDGE('',*,*,#10954,.T.);
#16390=ORIENTED_EDGE('',*,*,#10955,.F.);
#16391=ORIENTED_EDGE('',*,*,#10956,.T.);
#16392=ORIENTED_EDGE('',*,*,#10952,.T.);
#16393=ORIENTED_EDGE('',*,*,#10957,.T.);
#16394=ORIENTED_EDGE('',*,*,#10958,.F.);
#16395=ORIENTED_EDGE('',*,*,#10959,.T.);
#16396=ORIENTED_EDGE('',*,*,#10960,.T.);
#16397=ORIENTED_EDGE('',*,*,#10961,.F.);
#16398=ORIENTED_EDGE('',*,*,#10962,.F.);
#16399=ORIENTED_EDGE('',*,*,#10963,.T.);
#16400=ORIENTED_EDGE('',*,*,#10958,.T.);
#16401=ORIENTED_EDGE('',*,*,#10964,.F.);
#16402=ORIENTED_EDGE('',*,*,#10965,.F.);
#16403=ORIENTED_EDGE('',*,*,#10966,.T.);
#16404=ORIENTED_EDGE('',*,*,#10962,.T.);
#16405=ORIENTED_EDGE('',*,*,#10967,.F.);
#16406=ORIENTED_EDGE('',*,*,#10968,.F.);
#16407=ORIENTED_EDGE('',*,*,#10969,.T.);
#16408=ORIENTED_EDGE('',*,*,#10965,.T.);
#16409=ORIENTED_EDGE('',*,*,#10970,.F.);
#16410=ORIENTED_EDGE('',*,*,#10971,.F.);
#16411=ORIENTED_EDGE('',*,*,#10972,.T.);
#16412=ORIENTED_EDGE('',*,*,#10968,.T.);
#16413=ORIENTED_EDGE('',*,*,#10973,.F.);
#16414=ORIENTED_EDGE('',*,*,#10974,.F.);
#16415=ORIENTED_EDGE('',*,*,#10975,.T.);
#16416=ORIENTED_EDGE('',*,*,#10971,.T.);
#16417=ORIENTED_EDGE('',*,*,#10976,.F.);
#16418=ORIENTED_EDGE('',*,*,#10977,.F.);
#16419=ORIENTED_EDGE('',*,*,#10978,.T.);
#16420=ORIENTED_EDGE('',*,*,#10974,.T.);
#16421=ORIENTED_EDGE('',*,*,#10979,.F.);
#16422=ORIENTED_EDGE('',*,*,#10980,.F.);
#16423=ORIENTED_EDGE('',*,*,#10981,.T.);
#16424=ORIENTED_EDGE('',*,*,#10977,.T.);
#16425=ORIENTED_EDGE('',*,*,#10982,.F.);
#16426=ORIENTED_EDGE('',*,*,#10983,.F.);
#16427=ORIENTED_EDGE('',*,*,#10960,.F.);
#16428=ORIENTED_EDGE('',*,*,#10984,.F.);
#16429=ORIENTED_EDGE('',*,*,#10985,.F.);
#16430=ORIENTED_EDGE('',*,*,#10986,.F.);
#16431=ORIENTED_EDGE('',*,*,#10987,.T.);
#16432=ORIENTED_EDGE('',*,*,#10988,.F.);
#16433=ORIENTED_EDGE('',*,*,#10987,.F.);
#16434=ORIENTED_EDGE('',*,*,#10984,.T.);
#16435=ORIENTED_EDGE('',*,*,#10959,.F.);
#16436=ORIENTED_EDGE('',*,*,#10963,.F.);
#16437=ORIENTED_EDGE('',*,*,#10966,.F.);
#16438=ORIENTED_EDGE('',*,*,#10969,.F.);
#16439=ORIENTED_EDGE('',*,*,#10972,.F.);
#16440=ORIENTED_EDGE('',*,*,#10975,.F.);
#16441=ORIENTED_EDGE('',*,*,#10978,.F.);
#16442=ORIENTED_EDGE('',*,*,#10981,.F.);
#16443=ORIENTED_EDGE('',*,*,#10989,.F.);
#16444=ORIENTED_EDGE('',*,*,#10990,.F.);
#16445=ORIENTED_EDGE('',*,*,#10934,.F.);
#16446=ORIENTED_EDGE('',*,*,#10938,.F.);
#16447=ORIENTED_EDGE('',*,*,#10941,.F.);
#16448=ORIENTED_EDGE('',*,*,#10944,.F.);
#16449=ORIENTED_EDGE('',*,*,#10947,.F.);
#16450=ORIENTED_EDGE('',*,*,#10950,.F.);
#16451=ORIENTED_EDGE('',*,*,#10953,.F.);
#16452=ORIENTED_EDGE('',*,*,#10956,.F.);
#16453=ORIENTED_EDGE('',*,*,#10991,.F.);
#16454=ORIENTED_EDGE('',*,*,#10980,.T.);
#16455=ORIENTED_EDGE('',*,*,#10992,.F.);
#16456=ORIENTED_EDGE('',*,*,#10993,.F.);
#16457=ORIENTED_EDGE('',*,*,#10989,.T.);
#16458=ORIENTED_EDGE('',*,*,#10994,.F.);
#16459=ORIENTED_EDGE('',*,*,#10995,.T.);
#16460=ORIENTED_EDGE('',*,*,#10996,.T.);
#16461=ORIENTED_EDGE('',*,*,#10997,.F.);
#16462=ORIENTED_EDGE('',*,*,#10998,.F.);
#16463=ORIENTED_EDGE('',*,*,#10999,.T.);
#16464=ORIENTED_EDGE('',*,*,#11000,.T.);
#16465=ORIENTED_EDGE('',*,*,#10995,.F.);
#16466=ORIENTED_EDGE('',*,*,#11001,.F.);
#16467=ORIENTED_EDGE('',*,*,#11002,.T.);
#16468=ORIENTED_EDGE('',*,*,#11003,.T.);
#16469=ORIENTED_EDGE('',*,*,#10999,.F.);
#16470=ORIENTED_EDGE('',*,*,#11004,.F.);
#16471=ORIENTED_EDGE('',*,*,#11005,.T.);
#16472=ORIENTED_EDGE('',*,*,#11006,.T.);
#16473=ORIENTED_EDGE('',*,*,#11002,.F.);
#16474=ORIENTED_EDGE('',*,*,#11007,.F.);
#16475=ORIENTED_EDGE('',*,*,#11008,.T.);
#16476=ORIENTED_EDGE('',*,*,#11009,.T.);
#16477=ORIENTED_EDGE('',*,*,#11005,.F.);
#16478=ORIENTED_EDGE('',*,*,#11010,.F.);
#16479=ORIENTED_EDGE('',*,*,#10997,.T.);
#16480=ORIENTED_EDGE('',*,*,#11011,.T.);
#16481=ORIENTED_EDGE('',*,*,#11008,.F.);
#16482=ORIENTED_EDGE('',*,*,#11011,.F.);
#16483=ORIENTED_EDGE('',*,*,#10996,.F.);
#16484=ORIENTED_EDGE('',*,*,#11000,.F.);
#16485=ORIENTED_EDGE('',*,*,#11003,.F.);
#16486=ORIENTED_EDGE('',*,*,#11006,.F.);
#16487=ORIENTED_EDGE('',*,*,#11009,.F.);
#16488=ORIENTED_EDGE('',*,*,#10983,.T.);
#16489=ORIENTED_EDGE('',*,*,#10986,.T.);
#16490=ORIENTED_EDGE('',*,*,#11012,.F.);
#16491=ORIENTED_EDGE('',*,*,#10957,.F.);
#16492=ORIENTED_EDGE('',*,*,#10954,.F.);
#16493=ORIENTED_EDGE('',*,*,#10951,.F.);
#16494=ORIENTED_EDGE('',*,*,#10948,.F.);
#16495=ORIENTED_EDGE('',*,*,#10945,.F.);
#16496=ORIENTED_EDGE('',*,*,#10942,.F.);
#16497=ORIENTED_EDGE('',*,*,#10939,.F.);
#16498=ORIENTED_EDGE('',*,*,#10936,.F.);
#16499=ORIENTED_EDGE('',*,*,#11013,.F.);
#16500=ORIENTED_EDGE('',*,*,#10992,.T.);
#16501=ORIENTED_EDGE('',*,*,#10982,.T.);
#16502=ORIENTED_EDGE('',*,*,#10979,.T.);
#16503=ORIENTED_EDGE('',*,*,#10976,.T.);
#16504=ORIENTED_EDGE('',*,*,#10973,.T.);
#16505=ORIENTED_EDGE('',*,*,#10970,.T.);
#16506=ORIENTED_EDGE('',*,*,#10967,.T.);
#16507=ORIENTED_EDGE('',*,*,#10964,.T.);
#16508=ORIENTED_EDGE('',*,*,#10961,.T.);
#16509=ORIENTED_EDGE('',*,*,#11014,.T.);
#16510=ORIENTED_EDGE('',*,*,#11015,.T.);
#16511=ORIENTED_EDGE('',*,*,#10990,.T.);
#16512=ORIENTED_EDGE('',*,*,#10993,.T.);
#16513=ORIENTED_EDGE('',*,*,#11013,.T.);
#16514=ORIENTED_EDGE('',*,*,#10955,.T.);
#16515=ORIENTED_EDGE('',*,*,#11012,.T.);
#16516=ORIENTED_EDGE('',*,*,#10985,.T.);
#16517=ORIENTED_EDGE('',*,*,#10991,.T.);
#16518=ORIENTED_EDGE('',*,*,#11016,.F.);
#16519=ORIENTED_EDGE('',*,*,#10994,.T.);
#16520=ORIENTED_EDGE('',*,*,#11010,.T.);
#16521=ORIENTED_EDGE('',*,*,#11007,.T.);
#16522=ORIENTED_EDGE('',*,*,#11004,.T.);
#16523=ORIENTED_EDGE('',*,*,#11001,.T.);
#16524=ORIENTED_EDGE('',*,*,#10998,.T.);
#16525=ORIENTED_EDGE('',*,*,#11014,.F.);
#16526=ORIENTED_EDGE('',*,*,#10935,.F.);
#16527=ORIENTED_EDGE('',*,*,#11015,.F.);
#16528=ORIENTED_EDGE('',*,*,#11017,.T.);
#16529=ORIENTED_EDGE('',*,*,#11016,.T.);
#16530=ORIENTED_EDGE('',*,*,#11017,.F.);
#16531=ORIENTED_EDGE('',*,*,#10988,.T.);
#17255=CYLINDRICAL_SURFACE('',#19702,1.4635);
#17256=CYLINDRICAL_SURFACE('',#19704,1.4635);
#17257=CYLINDRICAL_SURFACE('',#19705,1.4635);
#17258=CYLINDRICAL_SURFACE('',#19706,1.4635);
#17259=CYLINDRICAL_SURFACE('',#19707,1.4635);
#17260=CYLINDRICAL_SURFACE('',#19708,1.4635);
#17261=CYLINDRICAL_SURFACE('',#19709,1.4635);
#17262=CYLINDRICAL_SURFACE('',#19710,1.4635);
#17263=CYLINDRICAL_SURFACE('',#19711,1.17775);
#17264=CYLINDRICAL_SURFACE('',#19713,1.17775);
#17265=CYLINDRICAL_SURFACE('',#19714,1.17775);
#17266=CYLINDRICAL_SURFACE('',#19715,1.17775);
#17267=CYLINDRICAL_SURFACE('',#19716,1.17775);
#17268=CYLINDRICAL_SURFACE('',#19717,1.17775);
#17269=CYLINDRICAL_SURFACE('',#19718,1.17775);
#17270=CYLINDRICAL_SURFACE('',#19719,1.17775);
#17271=CYLINDRICAL_SURFACE('',#19723,1.17775);
#17272=CYLINDRICAL_SURFACE('',#19735,1.4635);
#18238=ADVANCED_FACE('',(#1640),#17255,.T.);
#18239=ADVANCED_FACE('',(#1641),#17256,.T.);
#18240=ADVANCED_FACE('',(#1642),#17257,.T.);
#18241=ADVANCED_FACE('',(#1643),#17258,.T.);
#18242=ADVANCED_FACE('',(#1644),#17259,.T.);
#18243=ADVANCED_FACE('',(#1645),#17260,.T.);
#18244=ADVANCED_FACE('',(#1646),#17261,.T.);
#18245=ADVANCED_FACE('',(#1647),#17262,.T.);
#18246=ADVANCED_FACE('',(#1648),#17263,.T.);
#18247=ADVANCED_FACE('',(#1649),#17264,.T.);
#18248=ADVANCED_FACE('',(#1650),#17265,.T.);
#18249=ADVANCED_FACE('',(#1651),#17266,.T.);
#18250=ADVANCED_FACE('',(#1652),#17267,.T.);
#18251=ADVANCED_FACE('',(#1653),#17268,.T.);
#18252=ADVANCED_FACE('',(#1654),#17269,.T.);
#18253=ADVANCED_FACE('',(#1655),#17270,.T.);
#18254=ADVANCED_FACE('',(#1656),#254,.T.);
#18255=ADVANCED_FACE('',(#1657),#673,.F.);
#18256=ADVANCED_FACE('',(#1658),#17271,.T.);
#18257=ADVANCED_FACE('',(#1659),#604,.F.);
#18258=ADVANCED_FACE('',(#1660),#605,.F.);
#18259=ADVANCED_FACE('',(#1661),#606,.F.);
#18260=ADVANCED_FACE('',(#1662),#607,.F.);
#18261=ADVANCED_FACE('',(#1663),#608,.F.);
#18262=ADVANCED_FACE('',(#1664),#609,.F.);
#18263=ADVANCED_FACE('',(#1665),#610,.F.);
#18264=ADVANCED_FACE('',(#1666),#674,.F.);
#18265=ADVANCED_FACE('',(#1667),#611,.T.);
#18266=ADVANCED_FACE('',(#1668),#17272,.T.);
#18267=ADVANCED_FACE('',(#1669,#439),#612,.T.);
#18268=ADVANCED_FACE('',(#1670),#255,.T.);
#18269=ADVANCED_FACE('',(#1671),#613,.T.);
#18285=CLOSED_SHELL('',(#18238,#18239,#18240,#18241,#18242,#18243,#18244,
#18245,#18246,#18247,#18248,#18249,#18250,#18251,#18252,#18253,#18254,#18255,
#18256,#18257,#18258,#18259,#18260,#18261,#18262,#18263,#18264,#18265,#18266,
#18267,#18268,#18269));
#19701=AXIS2_PLACEMENT_3D('',#97841,#23143,#23144);
#19702=AXIS2_PLACEMENT_3D('',#97842,#23145,#23146);
#19703=AXIS2_PLACEMENT_3D('',#97858,#23148,#23149);
#19704=AXIS2_PLACEMENT_3D('',#97866,#23150,#23151);
#19705=AXIS2_PLACEMENT_3D('',#97914,#23153,#23154);
#19706=AXIS2_PLACEMENT_3D('',#97962,#23156,#23157);
#19707=AXIS2_PLACEMENT_3D('',#98010,#23159,#23160);
#19708=AXIS2_PLACEMENT_3D('',#98058,#23162,#23163);
#19709=AXIS2_PLACEMENT_3D('',#98106,#23165,#23166);
#19710=AXIS2_PLACEMENT_3D('',#98154,#23168,#23169);
#19711=AXIS2_PLACEMENT_3D('',#98208,#23171,#23172);
#19712=AXIS2_PLACEMENT_3D('',#98223,#23174,#23175);
#19713=AXIS2_PLACEMENT_3D('',#98232,#23176,#23177);
#19714=AXIS2_PLACEMENT_3D('',#98257,#23179,#23180);
#19715=AXIS2_PLACEMENT_3D('',#98282,#23182,#23183);
#19716=AXIS2_PLACEMENT_3D('',#98306,#23185,#23186);
#19717=AXIS2_PLACEMENT_3D('',#98330,#23188,#23189);
#19718=AXIS2_PLACEMENT_3D('',#98356,#23191,#23192);
#19719=AXIS2_PLACEMENT_3D('',#98380,#23194,#23195);
#19720=AXIS2_PLACEMENT_3D('',#98404,#23197,#23198);
#19721=AXIS2_PLACEMENT_3D('',#98653,#23199,#23200);
#19722=AXIS2_PLACEMENT_3D('',#98696,#23202,#23203);
#19723=AXIS2_PLACEMENT_3D('',#99032,#23204,#23205);
#19724=AXIS2_PLACEMENT_3D('',#99043,#23206,#23207);
#19725=AXIS2_PLACEMENT_3D('',#99044,#23208,#23209);
#19726=AXIS2_PLACEMENT_3D('',#99053,#23214,#23215);
#19727=AXIS2_PLACEMENT_3D('',#99059,#23219,#23220);
#19728=AXIS2_PLACEMENT_3D('',#99065,#23224,#23225);
#19729=AXIS2_PLACEMENT_3D('',#99071,#23229,#23230);
#19730=AXIS2_PLACEMENT_3D('',#99077,#23234,#23235);
#19731=AXIS2_PLACEMENT_3D('',#99080,#23238,#23239);
#19732=AXIS2_PLACEMENT_3D('',#99421,#23240,#23241);
#19733=AXIS2_PLACEMENT_3D('',#99423,#23242,#23243);
#19734=AXIS2_PLACEMENT_3D('',#99424,#23244,#23245);
#19735=AXIS2_PLACEMENT_3D('',#99425,#23246,#23247);
#19736=AXIS2_PLACEMENT_3D('',#99426,#23248,#23249);
#19737=AXIS2_PLACEMENT_3D('',#99428,#23250,#23251);
#19738=AXIS2_PLACEMENT_3D('',#99429,#23252,#23253);
#19739=AXIS2_PLACEMENT_3D('',#99431,#23255,#23256);
#23143=DIRECTION('axis',(0.,0.,1.));
#23144=DIRECTION('refdir',(1.,0.,0.));
#23145=DIRECTION('center_axis',(0.,0.,1.));
#23146=DIRECTION('ref_axis',(1.,0.,0.));
#23147=DIRECTION('',(0.,0.,-1.));
#23148=DIRECTION('center_axis',(0.,0.,-1.));
#23149=DIRECTION('ref_axis',(1.,0.,0.));
#23150=DIRECTION('center_axis',(0.,0.,1.));
#23151=DIRECTION('ref_axis',(1.,0.,0.));
#23152=DIRECTION('',(0.,0.,-1.));
#23153=DIRECTION('center_axis',(0.,0.,1.));
#23154=DIRECTION('ref_axis',(1.,0.,0.));
#23155=DIRECTION('',(0.,0.,-1.));
#23156=DIRECTION('center_axis',(0.,0.,1.));
#23157=DIRECTION('ref_axis',(1.,0.,0.));
#23158=DIRECTION('',(0.,0.,-1.));
#23159=DIRECTION('center_axis',(0.,0.,1.));
#23160=DIRECTION('ref_axis',(1.,0.,0.));
#23161=DIRECTION('',(0.,0.,-1.));
#23162=DIRECTION('center_axis',(0.,0.,1.));
#23163=DIRECTION('ref_axis',(1.,0.,0.));
#23164=DIRECTION('',(0.,0.,-1.));
#23165=DIRECTION('center_axis',(0.,0.,1.));
#23166=DIRECTION('ref_axis',(1.,0.,0.));
#23167=DIRECTION('',(0.,0.,-1.));
#23168=DIRECTION('center_axis',(0.,0.,1.));
#23169=DIRECTION('ref_axis',(1.,0.,0.));
#23170=DIRECTION('',(0.,0.,-1.));
#23171=DIRECTION('center_axis',(0.,0.,1.));
#23172=DIRECTION('ref_axis',(0.968655785309639,-0.24840686300134,0.));
#23173=DIRECTION('',(0.,0.,1.));
#23174=DIRECTION('center_axis',(0.,0.,-1.));
#23175=DIRECTION('ref_axis',(1.,4.0036529262094E-14,0.));
#23176=DIRECTION('center_axis',(0.,0.,1.));
#23177=DIRECTION('ref_axis',(1.,4.0036529262094E-14,0.));
#23178=DIRECTION('',(0.,0.,1.));
#23179=DIRECTION('center_axis',(0.,0.,1.));
#23180=DIRECTION('ref_axis',(1.,4.0036529262094E-14,0.));
#23181=DIRECTION('',(0.,0.,1.));
#23182=DIRECTION('center_axis',(0.,0.,1.));
#23183=DIRECTION('ref_axis',(1.,4.0036529262094E-14,0.));
#23184=DIRECTION('',(0.,0.,1.));
#23185=DIRECTION('center_axis',(0.,0.,1.));
#23186=DIRECTION('ref_axis',(1.,4.0036529262094E-14,0.));
#23187=DIRECTION('',(0.,0.,1.));
#23188=DIRECTION('center_axis',(0.,0.,1.));
#23189=DIRECTION('ref_axis',(1.,4.0036529262094E-14,0.));
#23190=DIRECTION('',(0.,0.,1.));
#23191=DIRECTION('center_axis',(0.,0.,1.));
#23192=DIRECTION('ref_axis',(1.,4.0036529262094E-14,0.));
#23193=DIRECTION('',(0.,0.,1.));
#23194=DIRECTION('center_axis',(0.,0.,1.));
#23195=DIRECTION('ref_axis',(1.,4.0036529262094E-14,0.));
#23196=DIRECTION('',(0.,0.,1.));
#23197=DIRECTION('center_axis',(0.,0.,-1.));
#23198=DIRECTION('ref_axis',(1.,0.,0.));
#23199=DIRECTION('center_axis',(0.,0.,-1.));
#23200=DIRECTION('ref_axis',(1.,0.,0.));
#23201=DIRECTION('',(0.707106781186548,8.65956056235494E-17,0.707106781186547));
#23202=DIRECTION('center_axis',(0.,0.,1.));
#23203=DIRECTION('ref_axis',(1.,0.,0.));
#23204=DIRECTION('center_axis',(0.,0.,1.));
#23205=DIRECTION('ref_axis',(1.,4.0036529262094E-14,0.));
#23206=DIRECTION('center_axis',(0.,0.,-1.));
#23207=DIRECTION('ref_axis',(1.,4.0036529262094E-14,0.));
#23208=DIRECTION('center_axis',(-2.40370335797945E-16,-1.,0.));
#23209=DIRECTION('ref_axis',(1.,-2.40370335797945E-16,0.));
#23210=DIRECTION('',(1.,-2.40370335797945E-16,0.));
#23211=DIRECTION('',(0.,0.,1.));
#23212=DIRECTION('',(1.,-2.40370335797945E-16,0.));
#23213=DIRECTION('',(0.,0.,1.));
#23214=DIRECTION('center_axis',(-0.866025403784439,-0.5,0.));
#23215=DIRECTION('ref_axis',(0.5,-0.866025403784439,0.));
#23216=DIRECTION('',(0.5,-0.866025403784439,0.));
#23217=DIRECTION('',(0.,0.,1.));
#23218=DIRECTION('',(0.5,-0.866025403784439,0.));
#23219=DIRECTION('center_axis',(-0.866025403784439,0.5,0.));
#23220=DIRECTION('ref_axis',(-0.5,-0.866025403784439,0.));
#23221=DIRECTION('',(-0.5,-0.866025403784439,0.));
#23222=DIRECTION('',(0.,0.,1.));
#23223=DIRECTION('',(-0.5,-0.866025403784439,0.));
#23224=DIRECTION('center_axis',(1.20185167898973E-16,1.,0.));
#23225=DIRECTION('ref_axis',(-1.,1.20185167898973E-16,0.));
#23226=DIRECTION('',(-1.,1.20185167898973E-16,0.));
#23227=DIRECTION('',(0.,0.,1.));
#23228=DIRECTION('',(-1.,1.20185167898973E-16,0.));
#23229=DIRECTION('center_axis',(0.866025403784439,0.5,0.));
#23230=DIRECTION('ref_axis',(-0.5,0.866025403784439,0.));
#23231=DIRECTION('',(-0.5,0.866025403784439,0.));
#23232=DIRECTION('',(0.,0.,1.));
#23233=DIRECTION('',(-0.5,0.866025403784439,0.));
#23234=DIRECTION('center_axis',(0.866025403784439,-0.5,0.));
#23235=DIRECTION('ref_axis',(0.5,0.866025403784439,0.));
#23236=DIRECTION('',(0.5,0.866025403784439,0.));
#23237=DIRECTION('',(0.5,0.866025403784439,0.));
#23238=DIRECTION('center_axis',(0.,0.,1.));
#23239=DIRECTION('ref_axis',(1.,0.,0.));
#23240=DIRECTION('center_axis',(0.,0.,1.));
#23241=DIRECTION('ref_axis',(1.,0.,0.));
#23242=DIRECTION('center_axis',(0.,0.,-1.));
#23243=DIRECTION('ref_axis',(1.,0.,0.));
#23244=DIRECTION('center_axis',(0.,0.,-1.));
#23245=DIRECTION('ref_axis',(1.,0.,0.));
#23246=DIRECTION('center_axis',(0.,0.,1.));
#23247=DIRECTION('ref_axis',(0.846289845614947,-0.532722720755394,0.));
#23248=DIRECTION('center_axis',(0.,0.,-1.));
#23249=DIRECTION('ref_axis',(-1.,0.,0.));
#23250=DIRECTION('center_axis',(0.,0.,1.));
#23251=DIRECTION('ref_axis',(1.,0.,0.));
#23252=DIRECTION('center_axis',(0.,0.,-1.));
#23253=DIRECTION('ref_axis',(1.,0.,0.));
#23254=DIRECTION('',(-0.707106781186548,-8.65956056235493E-17,-0.707106781186547));
#23255=DIRECTION('center_axis',(0.,0.,1.));
#23256=DIRECTION('ref_axis',(1.,0.,0.));
#97841=CARTESIAN_POINT('',(0.,0.,0.));
#97842=CARTESIAN_POINT('Origin',(0.,0.,1.5));
#97843=CARTESIAN_POINT('',(-1.46525529183604,0.000949695766822006,1.6971550458429));
#97844=CARTESIAN_POINT('',(-1.46480951624159,0.00160986999158072,1.62584495415709));
#97845=CARTESIAN_POINT('',(-1.4635,-1.79227059055215E-16,1.5));
#97846=CARTESIAN_POINT('',(0.634778394200743,1.31997491940301,1.5365));
#97847=CARTESIAN_POINT('Ctrl Pts',(-1.46525529183604,0.000949695766822006,
1.6971550458429));
#97848=CARTESIAN_POINT('Ctrl Pts',(-1.46560042360025,0.0508589123847686,
1.69443173840928));
#97849=CARTESIAN_POINT('Ctrl Pts',(-1.46327194301474,0.100733436630517,
1.69170843097565));
#97850=CARTESIAN_POINT('Ctrl Pts',(-1.45816376909485,0.150318972596548,
1.68898512354203));
#97851=CARTESIAN_POINT('Ctrl Pts',(-1.40854101969113,0.632011777869308,
1.66252987662845));
#97852=CARTESIAN_POINT('Ctrl Pts',(-1.09660082073563,1.08643298898876,1.63607462971487));
#97853=CARTESIAN_POINT('Ctrl Pts',(-0.664946563931385,1.30626231522188,
1.60961938280129));
#97854=CARTESIAN_POINT('Ctrl Pts',(-0.267264988146981,1.50879031415148,
1.58524625520086));
#97855=CARTESIAN_POINT('Ctrl Pts',(0.232028362605538,1.51219969455982,1.56087312760043));
#97856=CARTESIAN_POINT('Ctrl Pts',(0.635549693826274,1.32090956116917,1.5365));
#97857=CARTESIAN_POINT('',(-0.634007094575224,1.31904027763684,1.5365));
#97858=CARTESIAN_POINT('Origin',(0.,0.,1.5365));
#97859=CARTESIAN_POINT('Ctrl Pts',(-0.634007094575223,1.31904027763684,
1.5365));
#97860=CARTESIAN_POINT('Ctrl Pts',(-1.07313362622406,1.10797065284846,1.5629924276156));
#97861=CARTESIAN_POINT('Ctrl Pts',(-1.39474726964411,0.662191250162446,
1.5894848552312));
#97862=CARTESIAN_POINT('Ctrl Pts',(-1.45449093825341,0.181719547981815,
1.6159772828468));
#97863=CARTESIAN_POINT('Ctrl Pts',(-1.46190854066243,0.122065560563132,
1.6192665066169));
#97864=CARTESIAN_POINT('Ctrl Pts',(-1.46528941928426,0.0618767915960723,
1.622555730387));
#97865=CARTESIAN_POINT('Ctrl Pts',(-1.46480951624159,0.00160986999158072,
1.62584495415709));
#97866=CARTESIAN_POINT('Origin',(0.,0.,1.5));
#97867=CARTESIAN_POINT('',(-1.4614685241241,0.000737543191909745,2.19715504584291));
#97868=CARTESIAN_POINT('',(-1.46136527585292,0.000666719787592705,2.12584495415709));
#97869=CARTESIAN_POINT('',(-1.4635,-1.79227059055215E-16,1.5));
#97870=CARTESIAN_POINT('Ctrl Pts',(-1.4614685241241,0.000737543191909745,
2.19715504584291));
#97871=CARTESIAN_POINT('Ctrl Pts',(-1.46236405755613,0.197387960890566,
2.18649655322409));
#97872=CARTESIAN_POINT('Ctrl Pts',(-1.4254536386906,0.393715781199002,2.17583806060528));
#97873=CARTESIAN_POINT('Ctrl Pts',(-1.34914194794588,0.57329973733799,2.16517956798647));
#97874=CARTESIAN_POINT('Ctrl Pts',(-1.15973011521814,1.01904174526409,2.13872432107289));
#97875=CARTESIAN_POINT('Ctrl Pts',(-0.727577748980252,1.36162935416534,
2.11226907415931));
#97876=CARTESIAN_POINT('Ctrl Pts',(-0.250375545979114,1.4443538101403,2.08581382724573));
#97877=CARTESIAN_POINT('Ctrl Pts',(0.226826657022025,1.52707826611526,2.05935858033215));
#97878=CARTESIAN_POINT('Ctrl Pts',(0.749078696786409,1.34993956916391,2.03290333341857));
#97879=CARTESIAN_POINT('Ctrl Pts',(1.0774669053887,0.99394958746392,2.00644808650499));
#97880=CARTESIAN_POINT('Ctrl Pts',(1.40585511399099,0.637959605763926,1.97999283959141));
#97881=CARTESIAN_POINT('Ctrl Pts',(1.54037949143119,0.103118339315282,1.95353759267783));
#97882=CARTESIAN_POINT('Ctrl Pts',(1.41950779864889,-0.365863204421494,
1.92708234576425));
#97883=CARTESIAN_POINT('Ctrl Pts',(1.29863610586659,-0.834844748158274,
1.90062709885067));
#97884=CARTESIAN_POINT('Ctrl Pts',(0.922368342861785,-1.23796656918318,
1.87417185193709));
#97885=CARTESIAN_POINT('Ctrl Pts',(0.46281817834948,-1.39089651991568,1.84771660502351));
#97886=CARTESIAN_POINT('Ctrl Pts',(0.0032680138371783,-1.54382647064818,
1.82126135810993));
#97887=CARTESIAN_POINT('Ctrl Pts',(-0.539564552182622,-1.44656455108827,
1.79480611119635));
#97888=CARTESIAN_POINT('Ctrl Pts',(-0.917328185266559,-1.14345139159528,
1.76835086428277));
#97889=CARTESIAN_POINT('Ctrl Pts',(-1.25620476832629,-0.871540750195342,
1.74461892480281));
#97890=CARTESIAN_POINT('Ctrl Pts',(-1.46224768203056,-0.43397825017276,
1.72088698532286));
#97891=CARTESIAN_POINT('Ctrl Pts',(-1.46525529183604,0.000949695766822006,
1.6971550458429));
#97892=CARTESIAN_POINT('Ctrl Pts',(-1.46480951624159,0.00160986999158072,
1.62584495415709));
#97893=CARTESIAN_POINT('Ctrl Pts',(-1.46142413145071,-0.423531672472968,
1.6490481580026));
#97894=CARTESIAN_POINT('Ctrl Pts',(-1.2659135554708,-0.852562347168596,
1.6722513618481));
#97895=CARTESIAN_POINT('Ctrl Pts',(-0.940041506572989,-1.12518455749419,
1.6954545656936));
#97896=CARTESIAN_POINT('Ctrl Pts',(-0.567974712484741,-1.43645295911432,
1.72194699330921));
#97897=CARTESIAN_POINT('Ctrl Pts',(-0.0259674305097102,-1.54382576067933,
1.74843942092481));
#97898=CARTESIAN_POINT('Ctrl Pts',(0.437021120548429,-1.39911789592959,
1.77493184854041));
#97899=CARTESIAN_POINT('Ctrl Pts',(0.90000967160657,-1.25441003117985,1.80142427615601));
#97900=CARTESIAN_POINT('Ctrl Pts',(1.28397949174782,-0.857621500115369,
1.82791670377161));
#97901=CARTESIAN_POINT('Ctrl Pts',(1.41302018650067,-0.390197195079815,
1.85440913138721));
#97902=CARTESIAN_POINT('Ctrl Pts',(1.54206088125353,0.077227109955738,1.88090155900281));
#97903=CARTESIAN_POINT('Ctrl Pts',(1.41617245061799,0.615287188962364,1.90739398661841));
#97904=CARTESIAN_POINT('Ctrl Pts',(1.09299120959979,0.976927736970011,1.93388641423401));
#97905=CARTESIAN_POINT('Ctrl Pts',(0.769809968581594,1.33856828497766,1.96037884184961));
#97906=CARTESIAN_POINT('Ctrl Pts',(0.249335917180731,1.52378930198633,1.98687126946521));
#97907=CARTESIAN_POINT('Ctrl Pts',(-0.229668412333123,1.44778809968151,
2.01336369708081));
#97908=CARTESIAN_POINT('Ctrl Pts',(-0.708672741846977,1.37178689737668,
2.03985612469641));
#97909=CARTESIAN_POINT('Ctrl Pts',(-1.14620734947382,1.03456347575836,2.06634855231202));
#97910=CARTESIAN_POINT('Ctrl Pts',(-1.341629748858,0.590704472867507,2.09284097992762));
#97911=CARTESIAN_POINT('Ctrl Pts',(-1.42278143902801,0.40638625553278,2.10384230467077));
#97912=CARTESIAN_POINT('Ctrl Pts',(-1.46218248842652,0.203679441111252,
2.11484362941393));
#97913=CARTESIAN_POINT('Ctrl Pts',(-1.46136527585292,0.000666719787592705,
2.12584495415709));
#97914=CARTESIAN_POINT('Origin',(0.,0.,1.5));
#97915=CARTESIAN_POINT('',(-1.46259036218787,-0.00125761512241085,2.69715504584291));
#97916=CARTESIAN_POINT('',(-1.46263205222363,-0.00127650937794421,2.62584495415709));
#97917=CARTESIAN_POINT('',(-1.4635,-1.79227059055215E-16,1.5));
#97918=CARTESIAN_POINT('Ctrl Pts',(-1.46259036218787,-0.00125761512241085,
2.69715504584291));
#97919=CARTESIAN_POINT('Ctrl Pts',(-1.45978189217964,0.341135402893971,
2.67856136803891));
#97920=CARTESIAN_POINT('Ctrl Pts',(-1.33980853805453,0.685301349364496,
2.65996769023491));
#97921=CARTESIAN_POINT('Ctrl Pts',(-1.12026825930454,0.945438767331802,
2.64137401243091));
#97922=CARTESIAN_POINT('Ctrl Pts',(-0.807904436341066,1.31556455397457,
2.61491876551733));
#97923=CARTESIAN_POINT('Ctrl Pts',(-0.29397885919297,1.51558427707796,2.58846351860376));
#97924=CARTESIAN_POINT('Ctrl Pts',(0.186407751449748,1.45399701420947,2.56200827169017));
#97925=CARTESIAN_POINT('Ctrl Pts',(0.666794362092466,1.39240975134098,2.53555302477659));
#97926=CARTESIAN_POINT('Ctrl Pts',(1.1136420062298,1.0692155025006,2.50909777786301));
#97927=CARTESIAN_POINT('Ctrl Pts',(1.32253535862374,0.632262476730894,2.48264253094943));
#97928=CARTESIAN_POINT('Ctrl Pts',(1.53142871101768,0.195309450961193,2.45618728403585));
#97929=CARTESIAN_POINT('Ctrl Pts',(1.50236777166822,-0.355402351737828,
2.42973203712227));
#97930=CARTESIAN_POINT('Ctrl Pts',(1.24864693348105,-0.767943031297834,
2.40327679020869));
#97931=CARTESIAN_POINT('Ctrl Pts',(0.994926095293888,-1.18048371085784,
2.37682154329511));
#97932=CARTESIAN_POINT('Ctrl Pts',(0.516545358269026,-1.45485326727883,
2.35036629638153));
#97933=CARTESIAN_POINT('Ctrl Pts',(0.0323448230311008,-1.46554008895436,
2.32391104946795));
#97934=CARTESIAN_POINT('Ctrl Pts',(-0.451855712206826,-1.47622691062988,
2.29745580255437));
#97935=CARTESIAN_POINT('Ctrl Pts',(-0.941876045657816,-1.22323099755994,
2.27100055564079));
#97936=CARTESIAN_POINT('Ctrl Pts',(-1.21355056277452,-0.822284837549497,
2.24454530872721));
#97937=CARTESIAN_POINT('Ctrl Pts',(-1.37577076843208,-0.582874939172598,
2.22874855443244));
#97938=CARTESIAN_POINT('Ctrl Pts',(-1.46014127062829,-0.290714394849191,
2.21295180013767));
#97939=CARTESIAN_POINT('Ctrl Pts',(-1.4614685241241,0.000737543191909745,
2.19715504584291));
#97940=CARTESIAN_POINT('Ctrl Pts',(-1.46136527585292,0.000666719787592705,
2.12584495415709));
#97941=CARTESIAN_POINT('Ctrl Pts',(-1.46021454861399,-0.285198030491227,
2.14133605702953));
#97942=CARTESIAN_POINT('Ctrl Pts',(-1.37931982337241,-0.571669327104881,
2.15682715990198));
#97943=CARTESIAN_POINT('Ctrl Pts',(-1.22295946869643,-0.808260688939142,
2.17231826277442));
#97944=CARTESIAN_POINT('Ctrl Pts',(-0.955556598009147,-1.21287226369156,
2.19881069039002));
#97945=CARTESIAN_POINT('Ctrl Pts',(-0.46744066549306,-1.47160082903303,
2.22530311800562));
#97946=CARTESIAN_POINT('Ctrl Pts',(0.0175118003368193,-1.46580470042692,
2.25179554562122));
#97947=CARTESIAN_POINT('Ctrl Pts',(0.5024642661667,-1.4600085718208,2.27828797323682));
#97948=CARTESIAN_POINT('Ctrl Pts',(0.984253265310373,-1.18968774926711,
2.30478040085242));
#97949=CARTESIAN_POINT('Ctrl Pts',(1.24191574323231,-0.778810666555506,
2.33127282846802));
#97950=CARTESIAN_POINT('Ctrl Pts',(1.49957822115425,-0.367933583843902,
2.35776525608362));
#97951=CARTESIAN_POINT('Ctrl Pts',(1.53311417785445,0.18349975902561,2.38425768369922));
#97952=CARTESIAN_POINT('Ctrl Pts',(1.32714061082512,0.622574829610301,2.41075011131483));
#97953=CARTESIAN_POINT('Ctrl Pts',(1.1211670437958,1.06164990019499,2.43724253893043));
#97954=CARTESIAN_POINT('Ctrl Pts',(0.675683953036955,1.38836669849486,2.46373496654603));
#97955=CARTESIAN_POINT('Ctrl Pts',(0.195008236264954,1.45288333216258,2.49022739416163));
#97956=CARTESIAN_POINT('Ctrl Pts',(-0.285667480507048,1.5173999658303,2.51671982177723));
#97957=CARTESIAN_POINT('Ctrl Pts',(-0.801535823292203,1.31971643486587,
2.54321224939283));
#97958=CARTESIAN_POINT('Ctrl Pts',(-1.11600018720209,0.950496442197177,
2.56970467700843));
#97959=CARTESIAN_POINT('Ctrl Pts',(-1.33812801934386,0.689690939356804,
2.58841810272465));
#97960=CARTESIAN_POINT('Ctrl Pts',(-1.45976393507324,0.343296125582627,
2.60713152844087));
#97961=CARTESIAN_POINT('Ctrl Pts',(-1.46263205222363,-0.00127650937794421,
2.62584495415709));
#97962=CARTESIAN_POINT('Origin',(0.,0.,1.5));
#97963=CARTESIAN_POINT('',(-1.46589691679833,2.51587256358082E-5,3.19715504584291));
#97964=CARTESIAN_POINT('',(-1.4659121055392,-2.30038015023067E-5,3.12584495415709));
#97965=CARTESIAN_POINT('',(-1.4635,-1.79227059055215E-16,1.5));
#97966=CARTESIAN_POINT('Ctrl Pts',(-1.46589691679833,2.51587256358082E-5,
3.19715504584291));
#97967=CARTESIAN_POINT('Ctrl Pts',(-1.46602006156727,0.485691716639563,
3.17062618285372));
#97968=CARTESIAN_POINT('Ctrl Pts',(-1.20059041316976,0.971241251667598,
3.14409731986454));
#97969=CARTESIAN_POINT('Ctrl Pts',(-0.791886448608901,1.23360092154244,
3.11756845687536));
#97970=CARTESIAN_POINT('Ctrl Pts',(-0.384316614144986,1.49523255835758,
3.09111320996178));
#97971=CARTESIAN_POINT('Ctrl Pts',(0.165731625546887,1.53491129473518,3.0646579630482));
#97972=CARTESIAN_POINT('Ctrl Pts',(0.606632808874546,1.33448567256543,3.03820271613462));
#97973=CARTESIAN_POINT('Ctrl Pts',(1.0475339922022,1.13406005039567,3.01174746922104));
#97974=CARTESIAN_POINT('Ctrl Pts',(1.37928811916564,0.693530069678565,2.98529222230746));
#97975=CARTESIAN_POINT('Ctrl Pts',(1.45013070704306,0.21442088182498,2.95883697539388));
#97976=CARTESIAN_POINT('Ctrl Pts',(1.52097329492047,-0.264688306028604,
2.9323817284803));
#97977=CARTESIAN_POINT('Ctrl Pts',(1.33090434371185,-0.782376701018668,
2.90592648156672));
#97978=CARTESIAN_POINT('Ctrl Pts',(0.966872935492584,-1.10182217990777,
2.87947123465314));
#97979=CARTESIAN_POINT('Ctrl Pts',(0.602841527273315,-1.42126765879688,
2.85301598773956));
#97980=CARTESIAN_POINT('Ctrl Pts',(0.0648476620433925,-1.54247022158503,
2.82656074082597));
#97981=CARTESIAN_POINT('Ctrl Pts',(-0.400997606678097,-1.40998449219611,
2.80010549391239));
#97982=CARTESIAN_POINT('Ctrl Pts',(-0.866842875399587,-1.27749876280719,
2.77365024699881));
#97983=CARTESIAN_POINT('Ctrl Pts',(-1.26053954761264,-0.891324741241199,
2.74719500008523));
#97984=CARTESIAN_POINT('Ctrl Pts',(-1.40198684932975,-0.42812180536714,
2.72073975317166));
#97985=CARTESIAN_POINT('Ctrl Pts',(-1.44402001354272,-0.290474180907939,
2.71287818406207));
#97986=CARTESIAN_POINT('Ctrl Pts',(-1.46377780779679,-0.146024368754987,
2.70501661495249));
#97987=CARTESIAN_POINT('Ctrl Pts',(-1.46259036218787,-0.00125761512241085,
2.69715504584291));
#97988=CARTESIAN_POINT('Ctrl Pts',(-1.46263205222363,-0.00127650937794421,
2.62584495415709));
#97989=CARTESIAN_POINT('Ctrl Pts',(-1.46382430259504,-0.144512238767108,
2.63362395605647));
#97990=CARTESIAN_POINT('Ctrl Pts',(-1.44449359920879,-0.287433097526545,
2.64140295795585));
#97991=CARTESIAN_POINT('Ctrl Pts',(-1.40332716769488,-0.423760233432524,
2.64918195985523));
#97992=CARTESIAN_POINT('Ctrl Pts',(-1.26312939924317,-0.888040462020593,
2.67567438747083));
#97993=CARTESIAN_POINT('Ctrl Pts',(-0.869673477305141,-1.27584446482379,
2.70216681508643));
#97994=CARTESIAN_POINT('Ctrl Pts',(-0.403413676639095,-1.40931076214327,
2.72865924270203));
#97995=CARTESIAN_POINT('Ctrl Pts',(0.0628461240269517,-1.54277705946275,
2.75515167031764));
#97996=CARTESIAN_POINT('Ctrl Pts',(0.60190980342101,-1.42190565129851,2.78164409793324));
#97997=CARTESIAN_POINT('Ctrl Pts',(0.966541978861424,-1.1021326097128,2.80813652554884));
#97998=CARTESIAN_POINT('Ctrl Pts',(1.33117415430184,-0.782359568127089,
2.83462895316444));
#97999=CARTESIAN_POINT('Ctrl Pts',(1.5213748257886,-0.2636848931199,2.86112138078004));
#98000=CARTESIAN_POINT('Ctrl Pts',(1.44991055958715,0.216007011932497,2.88761380839564));
#98001=CARTESIAN_POINT('Ctrl Pts',(1.37844629338569,0.695698916984895,2.91410623601124));
#98002=CARTESIAN_POINT('Ctrl Pts',(1.04531708949601,1.1364080520825,2.94059866362684));
#98003=CARTESIAN_POINT('Ctrl Pts',(0.603308917416615,1.33600821530422,2.96709109124244));
#98004=CARTESIAN_POINT('Ctrl Pts',(0.161300745337218,1.53560837852595,2.99358351885804));
#98005=CARTESIAN_POINT('Ctrl Pts',(-0.389586394931897,1.49409956987179,
3.02007594647365));
#98006=CARTESIAN_POINT('Ctrl Pts',(-0.796694351740858,1.23051930167043,
3.04656837408925));
#98007=CARTESIAN_POINT('Ctrl Pts',(-1.20277424499078,0.967604648729325,
3.07299390077853));
#98008=CARTESIAN_POINT('Ctrl Pts',(-1.46580020468142,0.483738707465732,
3.09941942746781));
#98009=CARTESIAN_POINT('Ctrl Pts',(-1.4659121055392,-2.30038015023067E-5,
3.12584495415709));
#98010=CARTESIAN_POINT('Origin',(0.,0.,1.5));
#98011=CARTESIAN_POINT('',(-1.46251725547464,0.00124142858279441,3.69715504584291));
#98012=CARTESIAN_POINT('',(-1.46270047602225,0.00128924121849956,3.62584495415709));
#98013=CARTESIAN_POINT('',(-1.4635,-1.79227059055215E-16,1.5));
#98014=CARTESIAN_POINT('Ctrl Pts',(-1.46251725547464,0.00124142858279441,
3.69715504584291));
#98015=CARTESIAN_POINT('Ctrl Pts',(-1.46370702332812,0.148738027985318,
3.68914624458212));
#98016=CARTESIAN_POINT('Ctrl Pts',(-1.44318698960211,0.29591124700834,3.68113744332133));
#98017=CARTESIAN_POINT('Ctrl Pts',(-1.3995889627392,0.435896908748289,3.67312864206055));
#98018=CARTESIAN_POINT('Ctrl Pts',(-1.25557283247876,0.898307589835359,
3.64667339514697));
#98019=CARTESIAN_POINT('Ctrl Pts',(-0.859738774933637,1.28229049054632,
3.62021814823338));
#98020=CARTESIAN_POINT('Ctrl Pts',(-0.393165322540272,1.41218851737299,
3.5937629013198));
#98021=CARTESIAN_POINT('Ctrl Pts',(0.0734081298530866,1.54208654419966,
3.56730765440622));
#98022=CARTESIAN_POINT('Ctrl Pts',(0.610720977094688,1.41789969714205,3.54085240749265));
#98023=CARTESIAN_POINT('Ctrl Pts',(0.972973698680865,1.09643858054909,3.51439716057907));
#98024=CARTESIAN_POINT('Ctrl Pts',(1.33522642026705,0.774977463956125,3.48794191366548));
#98025=CARTESIAN_POINT('Ctrl Pts',(1.52241901619781,0.256242077827795,3.4614866667519));
#98026=CARTESIAN_POINT('Ctrl Pts',(1.44891822705338,-0.222466516044172,
3.43503141983832));
#98027=CARTESIAN_POINT('Ctrl Pts',(1.37541743790895,-0.701175109916134,
3.40857617292474));
#98028=CARTESIAN_POINT('Ctrl Pts',(1.04122326368934,-1.13985691153173,3.38212092601116));
#98029=CARTESIAN_POINT('Ctrl Pts',(0.599216411302075,-1.33783222868339,
3.35566567909758));
#98030=CARTESIAN_POINT('Ctrl Pts',(0.157209558914809,-1.53580754583504,
3.329210432184));
#98031=CARTESIAN_POINT('Ctrl Pts',(-0.392609971640119,-1.49307637852275,
3.30275518527042));
#98032=CARTESIAN_POINT('Ctrl Pts',(-0.798721343475862,-1.2291865579612,
3.27629993835684));
#98033=CARTESIAN_POINT('Ctrl Pts',(-1.2037026436268,-0.966031054227035,
3.24991830751886));
#98034=CARTESIAN_POINT('Ctrl Pts',(-1.46577445546874,-0.482946005415922,
3.22353667668088));
#98035=CARTESIAN_POINT('Ctrl Pts',(-1.46589691679833,2.51587256358082E-5,
3.19715504584291));
#98036=CARTESIAN_POINT('Ctrl Pts',(-1.4659121055392,-2.30038015023067E-5,
3.12584495415709));
#98037=CARTESIAN_POINT('Ctrl Pts',(-1.46602457299087,-0.486234172896521,
3.15240428269901));
#98038=CARTESIAN_POINT('Ctrl Pts',(-1.19994098143382,-0.972338508168191,
3.17896361124093));
#98039=CARTESIAN_POINT('Ctrl Pts',(-0.790477244895931,-1.23452231773249,
3.20552293978285));
#98040=CARTESIAN_POINT('Ctrl Pts',(-0.38204491633302,-1.49604570624368,
3.23201536739845));
#98041=CARTESIAN_POINT('Ctrl Pts',(0.169044599898504,-1.53477522966941,
3.25850779501405));
#98042=CARTESIAN_POINT('Ctrl Pts',(0.610040324245935,-1.33294802468893,
3.28500022262965));
#98043=CARTESIAN_POINT('Ctrl Pts',(1.05103604859337,-1.13112081970845,3.31149265024525));
#98044=CARTESIAN_POINT('Ctrl Pts',(1.3819379810567,-0.688736886321762,3.33798507786085));
#98045=CARTESIAN_POINT('Ctrl Pts',(1.45098168736653,-0.208690620830843,
3.36447750547645));
#98046=CARTESIAN_POINT('Ctrl Pts',(1.52002539367635,0.271355644660077,3.39096993309206));
#98047=CARTESIAN_POINT('Ctrl Pts',(1.32721087383265,0.789064242255226,3.41746236070766));
#98048=CARTESIAN_POINT('Ctrl Pts',(0.960970329747572,1.10699397323845,3.44395478832326));
#98049=CARTESIAN_POINT('Ctrl Pts',(0.594729785662495,1.42492370422168,3.47044721593886));
#98050=CARTESIAN_POINT('Ctrl Pts',(0.0550632173360358,1.54307456859298,
3.49693964355446));
#98051=CARTESIAN_POINT('Ctrl Pts',(-0.410517400180608,1.40725800636496,
3.52343207117006));
#98052=CARTESIAN_POINT('Ctrl Pts',(-0.876098017697253,1.27144144413694,
3.54992449878566));
#98053=CARTESIAN_POINT('Ctrl Pts',(-1.26759268440408,0.881657455309607,
3.57641692640127));
#98054=CARTESIAN_POINT('Ctrl Pts',(-1.40544679374999,0.416676063609308,
3.60290935401687));
#98055=CARTESIAN_POINT('Ctrl Pts',(-1.44522881216322,0.282491465310414,
3.61055455406361));
#98056=CARTESIAN_POINT('Ctrl Pts',(-1.46388796216068,0.142044521341646,
3.61819975411035));
#98057=CARTESIAN_POINT('Ctrl Pts',(-1.46270047602225,0.00128924121849956,
3.62584495415709));
#98058=CARTESIAN_POINT('Origin',(0.,0.,1.5));
#98059=CARTESIAN_POINT('',(-1.46151108967999,-0.00077281416562866,4.1971550458429));
#98060=CARTESIAN_POINT('',(-1.46133707147782,-0.000619497695943445,4.12584495415709));
#98061=CARTESIAN_POINT('',(-1.4635,-1.79227059055215E-16,1.5));
#98062=CARTESIAN_POINT('Ctrl Pts',(-1.46151108967999,-0.00077281416562866,
4.1971550458429));
#98063=CARTESIAN_POINT('Ctrl Pts',(-1.46010153861599,0.293373523763635,
4.18121105939693));
#98064=CARTESIAN_POINT('Ctrl Pts',(-1.3740385803959,0.588278752366279,4.16526707295096));
#98065=CARTESIAN_POINT('Ctrl Pts',(-1.20896762909038,0.829007033345531,
4.14932308650499));
#98066=CARTESIAN_POINT('Ctrl Pts',(-0.935071712918766,1.22843826304259,
4.12286783959141));
#98067=CARTESIAN_POINT('Ctrl Pts',(-0.443654974734093,1.47871225280756,
4.09641259267783));
#98068=CARTESIAN_POINT('Ctrl Pts',(0.040478713720523,1.46533847823884,4.06995734576425));
#98069=CARTESIAN_POINT('Ctrl Pts',(0.524612402175147,1.45196470367013,4.04350209885067));
#98070=CARTESIAN_POINT('Ctrl Pts',(1.00146304089972,1.17494316476773,4.01704685193709));
#98071=CARTESIAN_POINT('Ctrl Pts',(1.2528902039326,0.761000336383063,3.99059160502351));
#98072=CARTESIAN_POINT('Ctrl Pts',(1.50431736696549,0.347057507998399,3.96413635810993));
#98073=CARTESIAN_POINT('Ctrl Pts',(1.53032105430668,-0.203806609868528,
3.93768111119635));
#98074=CARTESIAN_POINT('Ctrl Pts',(1.31900559551541,-0.639593324011289,
3.91122586428277));
#98075=CARTESIAN_POINT('Ctrl Pts',(1.10769013672413,-1.07538003815405,3.88477061736919));
#98076=CARTESIAN_POINT('Ctrl Pts',(0.659055531800388,-1.39608934857265,
3.85831537045561));
#98077=CARTESIAN_POINT('Ctrl Pts',(0.17833449170055,-1.45500934316093,3.83186012354203));
#98078=CARTESIAN_POINT('Ctrl Pts',(-0.302386548399288,-1.51392933774921,
3.80540487662844));
#98079=CARTESIAN_POINT('Ctrl Pts',(-0.815194023675217,-1.31106001650717,
3.77894962971486));
#98080=CARTESIAN_POINT('Ctrl Pts',(-1.1254986598253,-0.93920612515456,3.75249438280128));
#98081=CARTESIAN_POINT('Ctrl Pts',(-1.34186472230247,-0.6799236236522,3.73404793714849));
#98082=CARTESIAN_POINT('Ctrl Pts',(-1.45977689679497,-0.338483321258646,
3.7156014914957));
#98083=CARTESIAN_POINT('Ctrl Pts',(-1.46251725547464,0.00124142858279441,
3.69715504584291));
#98084=CARTESIAN_POINT('Ctrl Pts',(-1.46270047602225,0.00128924121849956,
3.62584495415709));
#98085=CARTESIAN_POINT('Ctrl Pts',(-1.45977304163873,-0.345705838018082,
3.64469218172595));
#98086=CARTESIAN_POINT('Ctrl Pts',(-1.33622982194822,-0.694574796895743,
3.6635394092948));
#98087=CARTESIAN_POINT('Ctrl Pts',(-1.11119159617627,-0.956113418246287,
3.68238663686366));
#98088=CARTESIAN_POINT('Ctrl Pts',(-0.794868737271672,-1.32374271382832,
3.70887906447926));
#98089=CARTESIAN_POINT('Ctrl Pts',(-0.2780094674775,-1.51882251041912,3.73537149209487));
#98090=CARTESIAN_POINT('Ctrl Pts',(0.202334547739988,-1.45188166285187,
3.76186391971047));
#98091=CARTESIAN_POINT('Ctrl Pts',(0.682678562957472,-1.38494081528463,
3.78835634732607));
#98092=CARTESIAN_POINT('Ctrl Pts',(1.12650732359827,-1.05597932355936,3.81484877494167));
#98093=CARTESIAN_POINT('Ctrl Pts',(1.33026378228211,-0.615871659935628,
3.84134120255727));
#98094=CARTESIAN_POINT('Ctrl Pts',(1.53402024096595,-0.175763996311893,
3.86783363017287));
#98095=CARTESIAN_POINT('Ctrl Pts',(1.49770439769281,0.375489839210297,3.89432605778847));
#98096=CARTESIAN_POINT('Ctrl Pts',(1.23797210363236,0.785063502320118,3.92081848540407));
#98097=CARTESIAN_POINT('Ctrl Pts',(0.978239809571907,1.19463716542994,3.94731091301968));
#98098=CARTESIAN_POINT('Ctrl Pts',(0.495091064724133,1.46253065612739,3.97380334063527));
#98099=CARTESIAN_POINT('Ctrl Pts',(0.0101165833239452,1.46587765078508,
4.00029576825087));
#98100=CARTESIAN_POINT('Ctrl Pts',(-0.474857898076236,1.46922464544276,
4.02678819586647));
#98101=CARTESIAN_POINT('Ctrl Pts',(-0.961658116028831,1.20802514406069,
4.05328062348208));
#98102=CARTESIAN_POINT('Ctrl Pts',(-1.22701865007136,0.802075347968294,
4.07977305109768));
#98103=CARTESIAN_POINT('Ctrl Pts',(-1.38084455305005,0.566751756337598,
4.09513035211748));
#98104=CARTESIAN_POINT('Ctrl Pts',(-1.46025866906375,0.28278680150174,4.11048765313729));
#98105=CARTESIAN_POINT('Ctrl Pts',(-1.46133707147782,-0.000619497695943445,
4.12584495415709));
#98106=CARTESIAN_POINT('Origin',(0.,0.,1.5));
#98107=CARTESIAN_POINT('',(-1.46533193762214,-0.000810224173804775,4.6971550458429));
#98108=CARTESIAN_POINT('',(-1.46497413376758,-0.00101984791970569,4.62584495415709));
#98109=CARTESIAN_POINT('',(-1.4635,-1.79227059055215E-16,1.5));
#98110=CARTESIAN_POINT('Ctrl Pts',(-1.46533193762214,-0.000810224173804775,
4.6971550458429));
#98111=CARTESIAN_POINT('Ctrl Pts',(-1.46241910991127,0.436796001295317,
4.67327587421175));
#98112=CARTESIAN_POINT('Ctrl Pts',(-1.25345812331634,0.876815424349057,
4.64939670258059));
#98113=CARTESIAN_POINT('Ctrl Pts',(-0.910959994789205,1.14848054041163,
4.62551753094943));
#98114=CARTESIAN_POINT('Ctrl Pts',(-0.531513308045592,1.44945277823685,
4.59906228403586));
#98115=CARTESIAN_POINT('Ctrl Pts',(0.0118364913862525,1.54378741283756,
4.57260703712227));
#98116=CARTESIAN_POINT('Ctrl Pts',(0.470527355402032,1.38832979587355,4.54615179020869));
#98117=CARTESIAN_POINT('Ctrl Pts',(0.929218219417819,1.23287217890953,4.51969654329511));
#98118=CARTESIAN_POINT('Ctrl Pts',(1.30325014801754,0.827622310380775,4.49324129638153));
#98119=CARTESIAN_POINT('Ctrl Pts',(1.42151867773779,0.357966221832735,4.46678604946795));
#98120=CARTESIAN_POINT('Ctrl Pts',(1.53978720745805,-0.111689866715299,
4.44033080255437));
#98121=CARTESIAN_POINT('Ctrl Pts',(1.40229233829884,-0.645752175282618,
4.41387555564079));
#98122=CARTESIAN_POINT('Ctrl Pts',(1.07193233493599,-0.99990824823969,4.38742030872721));
#98123=CARTESIAN_POINT('Ctrl Pts',(0.741572331573142,-1.35406432119676,
4.36096506181363));
#98124=CARTESIAN_POINT('Ctrl Pts',(0.218347194006646,-1.52831415854358,
4.33450981490005));
#98125=CARTESIAN_POINT('Ctrl Pts',(-0.258388006446477,-1.44294526717024,
4.30805456798647));
#98126=CARTESIAN_POINT('Ctrl Pts',(-0.735123206899601,-1.35757637579689,
4.28159932107289));
#98127=CARTESIAN_POINT('Ctrl Pts',(-1.16536847023935,-1.01258875570338,
4.25514407415931));
#98128=CARTESIAN_POINT('Ctrl Pts',(-1.35230355482995,-0.565800710842041,
4.22868882724573));
#98129=CARTESIAN_POINT('Ctrl Pts',(-1.42657703906863,-0.388281841761277,
4.21817756677812));
#98130=CARTESIAN_POINT('Ctrl Pts',(-1.46244035278657,-0.194692244795154,
4.20766630631051));
#98131=CARTESIAN_POINT('Ctrl Pts',(-1.46151108967999,-0.00077281416562866,
4.1971550458429));
#98132=CARTESIAN_POINT('Ctrl Pts',(-1.46133707147782,-0.000619497695943445,
4.12584495415709));
#98133=CARTESIAN_POINT('Ctrl Pts',(-1.46211898930222,-0.206109057062041,
4.13698008075289));
#98134=CARTESIAN_POINT('Ctrl Pts',(-1.42171768447645,-0.411304915911804,
4.14811520734868));
#98135=CARTESIAN_POINT('Ctrl Pts',(-1.33863739786318,-0.597452549863065,
4.15925033394448));
#98136=CARTESIAN_POINT('Ctrl Pts',(-1.14097476147999,-1.04033056079928,
4.18574276156008));
#98137=CARTESIAN_POINT('Ctrl Pts',(-0.701728638581162,-1.37538649186899,
4.21223518917568));
#98138=CARTESIAN_POINT('Ctrl Pts',(-0.22235430315488,-1.44895072297049,
4.23872761679128));
#98139=CARTESIAN_POINT('Ctrl Pts',(0.257020032271406,-1.52251495407199,
4.26522004440688));
#98140=CARTESIAN_POINT('Ctrl Pts',(0.776522580225145,-1.33458748520527,
4.29171247202248));
#98141=CARTESIAN_POINT('Ctrl Pts',(1.09788936861022,-0.97135913130547,4.31820489963808));
#98142=CARTESIAN_POINT('Ctrl Pts',(1.41925615699529,-0.608130777405669,
4.34469732725369));
#98143=CARTESIAN_POINT('Ctrl Pts',(1.54248718581169,-0.0696015384727871,
4.37118975486929));
#98144=CARTESIAN_POINT('Ctrl Pts',(1.41106392995888,0.397238241529457,4.39768218248489));
#98145=CARTESIAN_POINT('Ctrl Pts',(1.27964067410607,0.864078021531702,4.42417461010049));
#98146=CARTESIAN_POINT('Ctrl Pts',(0.893563133584031,1.25922834260331,4.45066703771609));
#98147=CARTESIAN_POINT('Ctrl Pts',(0.429901422122667,1.40145795839054,4.47715946533169));
#98148=CARTESIAN_POINT('Ctrl Pts',(-0.0337602893386975,1.54368757417777,
4.50365189294729));
#98149=CARTESIAN_POINT('Ctrl Pts',(-0.575006171739392,1.43299648468063,
4.53014432056289));
#98150=CARTESIAN_POINT('Ctrl Pts',(-0.945599936232602,1.12015193692271,
4.55663674817849));
#98151=CARTESIAN_POINT('Ctrl Pts',(-1.26831013301763,0.847729313438621,
4.57970615017136));
#98152=CARTESIAN_POINT('Ctrl Pts',(-1.46161837309286,0.422017921110904,
4.60277555216422));
#98153=CARTESIAN_POINT('Ctrl Pts',(-1.46497413376758,-0.00101984791970569,
4.62584495415709));
#98154=CARTESIAN_POINT('Origin',(0.,0.,1.5));
#98155=CARTESIAN_POINT('',(-1.46394239258928,0.00129898642790893,5.19715504584291));
#98156=CARTESIAN_POINT('',(-1.46453843780727,0.00118155242986957,5.12584495415709));
#98157=CARTESIAN_POINT('',(-1.4635,-1.79227059055215E-16,1.5));
#98158=CARTESIAN_POINT('Ctrl Pts',(-1.46394239258928,0.00129898642790893,
5.19715504584291));
#98159=CARTESIAN_POINT('Ctrl Pts',(-1.46484061977216,0.0997535357056798,
5.19179593594014));
#98160=CARTESIAN_POINT('Ctrl Pts',(-1.455749977343,0.198041505549479,5.18643682603738));
#98161=CARTESIAN_POINT('Ctrl Pts',(-1.43605902275142,0.294156894358288,
5.18107771613462));
#98162=CARTESIAN_POINT('Ctrl Pts',(-1.33885462218189,0.768630526970514,
5.15462246922104));
#98163=CARTESIAN_POINT('Ctrl Pts',(-0.983330855508436,1.19016045875875,
5.12816722230746));
#98164=CARTESIAN_POINT('Ctrl Pts',(-0.532047870296871,1.36593679886265,
5.10171197539388));
#98165=CARTESIAN_POINT('Ctrl Pts',(-0.0807648850853061,1.54171313896655,
5.0752567284803));
#98166=CARTESIAN_POINT('Ctrl Pts',(0.466277318664373,1.47173588738613,5.04880148156672));
#98167=CARTESIAN_POINT('Ctrl Pts',(0.858787460264104,1.18800455079967,5.02234623465314));
#98168=CARTESIAN_POINT('Ctrl Pts',(1.25129760186384,0.904273214213206,4.99589098773956));
#98169=CARTESIAN_POINT('Ctrl Pts',(1.48927568131362,0.406787792620698,4.96943574082598));
#98170=CARTESIAN_POINT('Ctrl Pts',(1.46387758514864,-0.0768651975248075,
4.9429804939124));
#98171=CARTESIAN_POINT('Ctrl Pts',(1.43847948898366,-0.560518187670316,
4.91652524699882));
#98172=CARTESIAN_POINT('Ctrl Pts',(1.14970521720391,-1.03033874636882,4.89007000008524));
#98173=CARTESIAN_POINT('Ctrl Pts',(0.729646360262873,-1.27140582564898,
4.86361475317166));
#98174=CARTESIAN_POINT('Ctrl Pts',(0.309587503321841,-1.51247290492914,
4.83715950625807));
#98175=CARTESIAN_POINT('Ctrl Pts',(-0.241755938780478,-1.52478650479095,
4.81070425934449));
#98176=CARTESIAN_POINT('Ctrl Pts',(-0.672160067958435,-1.30271185053191,
4.78424901243091));
#98177=CARTESIAN_POINT('Ctrl Pts',(-1.10256419713639,-1.08063719627286,
4.75779376551733));
#98178=CARTESIAN_POINT('Ctrl Pts',(-1.41202901338999,-0.624174287892957,
4.73133851860375));
#98179=CARTESIAN_POINT('Ctrl Pts',(-1.45898963448909,-0.14213791317814,
4.70488327169017));
#98180=CARTESIAN_POINT('Ctrl Pts',(-1.46356241718342,-0.0951997011029249,
4.70230719640775));
#98181=CARTESIAN_POINT('Ctrl Pts',(-1.46564617228588,-0.0480190050426819,
4.69973112112533));
#98182=CARTESIAN_POINT('Ctrl Pts',(-1.46533193762214,-0.000810224173804775,
4.6971550458429));
#98183=CARTESIAN_POINT('Ctrl Pts',(-1.46497413376758,-0.00101984791970569,
4.62584495415709));
#98184=CARTESIAN_POINT('Ctrl Pts',(-1.4654720597553,-0.0637899675449887,
4.62926797977982));
#98185=CARTESIAN_POINT('Ctrl Pts',(-1.46178790327085,-0.126501223431492,
4.63269100540256));
#98186=CARTESIAN_POINT('Ctrl Pts',(-1.45372385837108,-0.188644118935721,
4.63611403102529));
#98187=CARTESIAN_POINT('Ctrl Pts',(-1.39131236943062,-0.669597621017519,
4.66260645864089));
#98188=CARTESIAN_POINT('Ctrl Pts',(-1.06654774496397,-1.11650661916241,
4.6890988862565));
#98189=CARTESIAN_POINT('Ctrl Pts',(-0.628379687548205,-1.32440124379681,
4.7155913138721));
#98190=CARTESIAN_POINT('Ctrl Pts',(-0.190211630132438,-1.5322958684312,
4.7420837414877));
#98191=CARTESIAN_POINT('Ctrl Pts',(0.361359860232456,-1.5011761195551,4.7685761691033));
#98192=CARTESIAN_POINT('Ctrl Pts',(0.773362895386055,-1.24531492034441,
4.7950685967189));
#98193=CARTESIAN_POINT('Ctrl Pts',(1.18536593053966,-0.989453721133718,
4.8215610243345));
#98194=CARTESIAN_POINT('Ctrl Pts',(1.45780051048196,-0.50885107158843,4.8480534519501));
#98195=CARTESIAN_POINT('Ctrl Pts',(1.46571731620589,-0.0239295633793579,
4.8745458795657));
#98196=CARTESIAN_POINT('Ctrl Pts',(1.47363412192982,0.460991944829711,4.9010383071813));
#98197=CARTESIAN_POINT('Ctrl Pts',(1.21703315343537,0.950232311702564,4.9275307347969));
#98198=CARTESIAN_POINT('Ctrl Pts',(0.813602072710932,1.21940623737337,4.9540231624125));
#98199=CARTESIAN_POINT('Ctrl Pts',(0.410170991986497,1.48858016304417,4.9805155900281));
#98200=CARTESIAN_POINT('Ctrl Pts',(-0.140090200967923,1.53768764751291,
5.0070080176437));
#98201=CARTESIAN_POINT('Ctrl Pts',(-0.584811428509822,1.3442074922315,5.03350044525931));
#98202=CARTESIAN_POINT('Ctrl Pts',(-1.02953265605172,1.15072733695009,5.05999287287491));
#98203=CARTESIAN_POINT('Ctrl Pts',(-1.3687139181811,0.714659541918519,5.08648530049051));
#98204=CARTESIAN_POINT('Ctrl Pts',(-1.44679165122832,0.235999019704764,
5.11297772810611));
#98205=CARTESIAN_POINT('Ctrl Pts',(-1.45943229273847,0.158504760711557,
5.11726680345644));
#98206=CARTESIAN_POINT('Ctrl Pts',(-1.46522914572839,0.0798941031068154,
5.12155587880677));
#98207=CARTESIAN_POINT('Ctrl Pts',(-1.46453843780727,0.00118155242986957,
5.12584495415709));
#98208=CARTESIAN_POINT('Origin',(0.,0.,0.612132885263843));
#98209=CARTESIAN_POINT('',(-1.17810601494501,0.00104535788546833,5.36213288526384));
#98210=CARTESIAN_POINT('',(-1.17585338136642,0.000266266979346078,5.46086711473616));
#98211=CARTESIAN_POINT('',(-1.17775,-4.72972551152008E-14,0.612132885263843));
#98212=CARTESIAN_POINT('',(-1.03290409957988,0.565865870654066,5.82225));
#98213=CARTESIAN_POINT('Ctrl Pts',(-1.17810601494501,0.00104535788546838,
5.36213288526384));
#98214=CARTESIAN_POINT('Ctrl Pts',(-1.17526052631953,-0.310848231437392,
5.38322902227466));
#98215=CARTESIAN_POINT('Ctrl Pts',(-0.888072305685325,-1.01854893491326,
5.43078040619906));
#98216=CARTESIAN_POINT('Ctrl Pts',(0.306526164541481,-1.35774082866675,
5.50478703703704));
#98217=CARTESIAN_POINT('Ctrl Pts',(1.30628459189527,-0.479538774867528,
5.58415277777777));
#98218=CARTESIAN_POINT('Ctrl Pts',(1.11262400044309,0.837919826534893,5.66351851851852));
#98219=CARTESIAN_POINT('Ctrl Pts',(-0.102449444944844,1.38774658789174,
5.74288425925926));
#98220=CARTESIAN_POINT('Ctrl Pts',(-0.844784006828786,0.909251158746022,
5.79579475308642));
#98221=CARTESIAN_POINT('Ctrl Pts',(-1.03290409957988,0.565865870654058,
5.82225));
#98222=CARTESIAN_POINT('',(0.200551794415749,1.1605490253568,5.82225));
#98223=CARTESIAN_POINT('Origin',(0.,0.,5.82225));
#98224=CARTESIAN_POINT('Ctrl Pts',(-1.17585338136642,0.000266266979346078,
5.46086711473616));
#98225=CARTESIAN_POINT('Ctrl Pts',(-1.17534105488343,-0.215031411505098,
5.47535836602837));
#98226=CARTESIAN_POINT('Ctrl Pts',(-1.01554696283918,-0.824585838872987,
5.51634204493618));
#98227=CARTESIAN_POINT('Ctrl Pts',(-0.0361513007060795,-1.39171212292046,
5.58381815145959));
#98228=CARTESIAN_POINT('Ctrl Pts',(1.15165463117661,-0.784596477531957,
5.66329543430639));
#98229=CARTESIAN_POINT('Ctrl Pts',(1.28099440281734,0.545166701406554,5.7427727171532));
#98230=CARTESIAN_POINT('Ctrl Pts',(0.586914422573267,1.09378259267779,5.7957575723844));
#98231=CARTESIAN_POINT('Ctrl Pts',(0.200551794415766,1.1605490253568,5.82225));
#98232=CARTESIAN_POINT('Origin',(0.,0.,0.612132885263843));
#98233=CARTESIAN_POINT('',(-1.17922424976732,-0.000652027004295064,4.86213288526384));
#98234=CARTESIAN_POINT('',(-1.17858568167237,0.000950853005947522,4.96086711473616));
#98235=CARTESIAN_POINT('',(-1.17775,-4.72972551152008E-14,0.612132885263843));
#98236=CARTESIAN_POINT('Ctrl Pts',(-1.17922424976732,-0.000652027004295177,
4.86213288526384));
#98237=CARTESIAN_POINT('Ctrl Pts',(-1.17947712976405,-0.0386432409901481,
4.86470896054627));
#98238=CARTESIAN_POINT('Ctrl Pts',(-1.16057915226501,-0.46653408645719,
4.89374028274227));
#98239=CARTESIAN_POINT('Ctrl Pts',(-0.63824584614602,-1.2369796024973,4.94922685185185));
#98240=CARTESIAN_POINT('Ctrl Pts',(0.692833222393801,-1.20725153504819,
5.0285925925926));
#98241=CARTESIAN_POINT('Ctrl Pts',(1.39000554611486,-0.0729888162087741,
5.10795833333333));
#98242=CARTESIAN_POINT('Ctrl Pts',(0.815467760521459,1.12806370571929,5.18732407407407));
#98243=CARTESIAN_POINT('Ctrl Pts',(-0.505227057653176,1.2970060522492,5.26668981481481));
#98244=CARTESIAN_POINT('Ctrl Pts',(-1.13539930062689,0.549836699603529,
5.32495941854474));
#98245=CARTESIAN_POINT('Ctrl Pts',(-1.17882886227309,0.080276547097573,
5.35677377536108));
#98246=CARTESIAN_POINT('Ctrl Pts',(-1.17810601494501,0.00104535788546838,
5.36213288526384));
#98247=CARTESIAN_POINT('Ctrl Pts',(-1.17858568167237,0.000950853005947504,
4.96086711473616));
#98248=CARTESIAN_POINT('Ctrl Pts',(-1.17570821901659,-0.326962608221022,
4.98307046700143));
#98249=CARTESIAN_POINT('Ctrl Pts',(-0.862548697969744,-1.05095270842858,
5.03176624688231));
#98250=CARTESIAN_POINT('Ctrl Pts',(0.364714346074539,-1.34397271822316,
5.10695445437878));
#98251=CARTESIAN_POINT('Ctrl Pts',(1.32746371769155,-0.420942597676582,
5.18643173722558));
#98252=CARTESIAN_POINT('Ctrl Pts',(1.07251885993521,0.888266730679483,5.26590902007238));
#98253=CARTESIAN_POINT('Ctrl Pts',(-0.166143802083737,1.38257845674616,
5.34538630291918));
#98254=CARTESIAN_POINT('Ctrl Pts',(-1.0544698941532,0.749960489548073,5.41037233447378));
#98255=CARTESIAN_POINT('Ctrl Pts',(-1.17627767326045,0.178568702663258,
5.44886593841277));
#98256=CARTESIAN_POINT('Ctrl Pts',(-1.17585338136642,0.000266266979346078,
5.46086711473616));
#98257=CARTESIAN_POINT('Origin',(0.,0.,0.612132885263843));
#98258=CARTESIAN_POINT('',(-1.17614942662836,-0.000621921341728721,4.36213288526384));
#98259=CARTESIAN_POINT('',(-1.17893630751266,-0.00082072148104434,4.46086711473616));
#98260=CARTESIAN_POINT('',(-1.17775,-4.72972551152008E-14,0.612132885263843));
#98261=CARTESIAN_POINT('Ctrl Pts',(-1.17614942662836,-0.000621921341728629,
4.36213288526384));
#98262=CARTESIAN_POINT('Ctrl Pts',(-1.17689725008157,-0.156678367822023,
4.37264414573145));
#98263=CARTESIAN_POINT('Ctrl Pts',(-1.07539762839906,-0.70457171109385,
4.40961065311264));
#98264=CARTESIAN_POINT('Ctrl Pts',(-0.245350186557975,-1.37013648524764,
4.47303240740741));
#98265=CARTESIAN_POINT('Ctrl Pts',(1.01784435891986,-0.949454395868983,
4.55239814814815));
#98266=CARTESIAN_POINT('Ctrl Pts',(1.3497908887844,0.339903753598391,4.63176388888888));
#98267=CARTESIAN_POINT('Ctrl Pts',(0.446785551083708,1.31827689878403,4.71112962962963));
#98268=CARTESIAN_POINT('Ctrl Pts',(-0.822416757865382,1.09792209940012,
4.78791929508794));
#98269=CARTESIAN_POINT('Ctrl Pts',(-1.17688015490128,0.351511097045095,
4.83825371363268));
#98270=CARTESIAN_POINT('Ctrl Pts',(-1.17922424976732,-0.000652027004295177,
4.86213288526384));
#98271=CARTESIAN_POINT('Ctrl Pts',(-1.17893630751266,-0.000820721481044288,
4.46086711473616));
#98272=CARTESIAN_POINT('Ctrl Pts',(-1.1793370128984,-0.0513349055525556,
4.46429014035889));
#98273=CARTESIAN_POINT('Ctrl Pts',(-1.15342602975686,-0.492388454964942,
4.49420559359722));
#98274=CARTESIAN_POINT('Ctrl Pts',(-0.596949142579923,-1.25815698208656,
4.55061347445117));
#98275=CARTESIAN_POINT('Ctrl Pts',(0.734680490718179,-1.18302623202404,
4.63009075729796));
#98276=CARTESIAN_POINT('Ctrl Pts',(1.39240476784912,-0.0227328862735182,
4.70956804014477));
#98277=CARTESIAN_POINT('Ctrl Pts',(0.772906734413495,1.15841403976235,4.78904532299156));
#98278=CARTESIAN_POINT('Ctrl Pts',(-0.555559517726036,1.27697162056126,
4.86852260583837));
#98279=CARTESIAN_POINT('Ctrl Pts',(-1.14566203930557,0.518307348212367,
4.9257965364199));
#98280=CARTESIAN_POINT('Ctrl Pts',(-1.17914152810497,0.0642946907646066,
4.95657803938583));
#98281=CARTESIAN_POINT('Ctrl Pts',(-1.17858568167237,0.000950853005947504,
4.96086711473616));
#98282=CARTESIAN_POINT('Origin',(0.,0.,0.612132885263843));
#98283=CARTESIAN_POINT('',(-1.17695913743441,0.000999038273554803,3.86213288526384));
#98284=CARTESIAN_POINT('',(-1.17600938567339,-0.000498540082993076,3.96086711473616));
#98285=CARTESIAN_POINT('',(-1.17775,-4.72972551152008E-14,0.612132885263843));
#98286=CARTESIAN_POINT('Ctrl Pts',(-1.17695913743441,0.000999038273554707,
3.86213288526384));
#98287=CARTESIAN_POINT('Ctrl Pts',(-1.1747538368297,-0.272394076947318,
3.88057933091664));
#98288=CARTESIAN_POINT('Ctrl Pts',(-0.943776669976225,-0.941238613449934,
3.92548102348301));
#98289=CARTESIAN_POINT('Ctrl Pts',(0.169336007262713,-1.38159181457256,
3.99683796296296));
#98290=CARTESIAN_POINT('Ctrl Pts',(1.25245060777301,-0.607320430195027,
4.0762037037037));
#98291=CARTESIAN_POINT('Ctrl Pts',(1.18967129222925,0.72260143140615,4.15556944444444));
#98292=CARTESIAN_POINT('Ctrl Pts',(0.0384362261044693,1.39139975892709,
4.23493518518518));
#98293=CARTESIAN_POINT('Ctrl Pts',(-0.990837095837684,0.867200396502629,
4.30378966545832));
#98294=CARTESIAN_POINT('Ctrl Pts',(-1.17501509197471,0.236092017500911,
4.34618889881787));
#98295=CARTESIAN_POINT('Ctrl Pts',(-1.17614942662836,-0.000621921341728629,
4.36213288526384));
#98296=CARTESIAN_POINT('Ctrl Pts',(-1.17600938567339,-0.000498540082993007,
3.96086711473616));
#98297=CARTESIAN_POINT('Ctrl Pts',(-1.17663863317436,-0.165866034817124,
3.97200224133195));
#98298=CARTESIAN_POINT('Ctrl Pts',(-1.0667717993835,-0.723873243149682,
4.00962979554334));
#98299=CARTESIAN_POINT('Ctrl Pts',(-0.211232513047386,-1.37647664066694,
4.07374977737036));
#98300=CARTESIAN_POINT('Ctrl Pts',(1.042974782858,-0.922773374952316,4.15322706021714));
#98301=CARTESIAN_POINT('Ctrl Pts',(1.34048488368858,0.37736904627051,4.23270434306396));
#98302=CARTESIAN_POINT('Ctrl Pts',(0.40839846752904,1.33135939264991,4.31218162591074));
#98303=CARTESIAN_POINT('Ctrl Pts',(-0.842023988191156,1.07563343065007,
4.38823588313483));
#98304=CARTESIAN_POINT('Ctrl Pts',(-1.17623576283577,0.339618453425564,
4.43779771274329));
#98305=CARTESIAN_POINT('Ctrl Pts',(-1.17893630751266,-0.000820721481044288,
4.46086711473616));
#98306=CARTESIAN_POINT('Origin',(0.,0.,0.612132885263843));
#98307=CARTESIAN_POINT('',(-1.17967891613203,2.02464564948595E-5,3.36213288526384));
#98308=CARTESIAN_POINT('',(-1.17710658396666,0.00103751543904164,3.46086711473616));
#98309=CARTESIAN_POINT('',(-1.17775,-4.72972551152008E-14,0.612132885263843));
#98310=CARTESIAN_POINT('Ctrl Pts',(-1.17967891613203,2.02464564948851E-5,
3.36213288526384));
#98311=CARTESIAN_POINT('Ctrl Pts',(-1.17958036551302,-0.388650261618471,
3.38851451610182));
#98312=CARTESIAN_POINT('Ctrl Pts',(-0.75718785921875,-1.16725938820271,
3.44135139385338));
#98313=CARTESIAN_POINT('Ctrl Pts',(0.568980874699694,-1.27032727667186,
3.52064351851852));
#98314=CARTESIAN_POINT('Ctrl Pts',(1.37580804658996,-0.211241198394891,
3.60000925925926));
#98315=CARTESIAN_POINT('Ctrl Pts',(0.92387894541309,1.04111397962895,3.679375));
#98316=CARTESIAN_POINT('Ctrl Pts',(-0.373326806220943,1.34093166146447,
3.75874074074074));
#98317=CARTESIAN_POINT('Ctrl Pts',(-1.10685463418829,0.629365443838005,
3.81966003582869));
#98318=CARTESIAN_POINT('Ctrl Pts',(-1.17791660179344,0.119696762869613,
3.85412408400306));
#98319=CARTESIAN_POINT('Ctrl Pts',(-1.17695913743441,0.000999038273554707,
3.86213288526384));
#98320=CARTESIAN_POINT('Ctrl Pts',(-1.17710658396666,0.00103751543904167,
3.46086711473616));
#98321=CARTESIAN_POINT('Ctrl Pts',(-1.174750734397,-0.278206389289945,3.47971434230502));
#98322=CARTESIAN_POINT('Ctrl Pts',(-0.935578896943687,-0.953594566271338,
3.52505399748947));
#98323=CARTESIAN_POINT('Ctrl Pts',(0.192214113207023,-1.37926097853155,
3.59688608028953));
#98324=CARTESIAN_POINT('Ctrl Pts',(1.26372622016576,-0.585066792922831,
3.67636336313633));
#98325=CARTESIAN_POINT('Ctrl Pts',(1.17605081651368,0.745795943229381,3.75584064598314));
#98326=CARTESIAN_POINT('Ctrl Pts',(0.00961056866032201,1.39255691077756,
3.83531792882993));
#98327=CARTESIAN_POINT('Ctrl Pts',(-1.00098658511986,0.850306798861559,
3.90366008508095));
#98328=CARTESIAN_POINT('Ctrl Pts',(-1.17514154252808,0.227572364515632,
3.94550981371635));
#98329=CARTESIAN_POINT('Ctrl Pts',(-1.17600938567339,-0.000498540082993007,
3.96086711473616));
#98330=CARTESIAN_POINT('Origin',(0.,0.,0.612132885263843));
#98331=CARTESIAN_POINT('',(-1.17701796998071,-0.00101206437339089,2.86213288526384));
#98332=CARTESIAN_POINT('',(-1.17969113925438,-1.85122837467744E-5,2.96086711473616));
#98333=CARTESIAN_POINT('',(-1.17775,-4.72972551152008E-14,0.612132885263843));
#98334=CARTESIAN_POINT('Ctrl Pts',(-1.17701796998071,-0.00101206437339095,
2.86213288526384));
#98335=CARTESIAN_POINT('Ctrl Pts',(-1.177973565516,-0.117512948617163,2.86999445437342));
#98336=CARTESIAN_POINT('Ctrl Pts',(-1.10856763284462,-0.624941754067655,
2.90431127039659));
#98337=CARTESIAN_POINT('Ctrl Pts',(-0.380763881655566,-1.33883882596208,
2.96508333333333));
#98338=CARTESIAN_POINT('Ctrl Pts',(0.918086015388248,-1.04622594248328,
3.04444907407407));
#98339=CARTESIAN_POINT('Ctrl Pts',(1.37695934771338,0.203601540672618,3.12381481481481));
#98340=CARTESIAN_POINT('Ctrl Pts',(0.576023051783349,1.26714957918899,3.20318055555555));
#98341=CARTESIAN_POINT('Ctrl Pts',(-0.751929078651436,1.17135532206144,
3.2825462962963));
#98342=CARTESIAN_POINT('Ctrl Pts',(-1.17918677678639,0.39194417008362,3.33553040619906));
#98343=CARTESIAN_POINT('Ctrl Pts',(-1.17967919113057,0.00110480402923826,
3.36205926918824));
#98344=CARTESIAN_POINT('Ctrl Pts',(-1.17967891613203,2.02464564948851E-5,
3.36213288526384));
#98345=CARTESIAN_POINT('Ctrl Pts',(-1.17969113925438,-1.85122837469034E-5,
2.96086711473616));
#98346=CARTESIAN_POINT('Ctrl Pts',(-1.17969136723729,-0.00100411151731483,
2.96093401566248));
#98347=CARTESIAN_POINT('Ctrl Pts',(-1.17924351116644,-0.392281796551246,
2.9874933442044));
#98348=CARTESIAN_POINT('Ctrl Pts',(-0.750938898498722,-1.17277357998896,
3.04054510036192));
#98349=CARTESIAN_POINT('Ctrl Pts',(0.579527130353369,-1.26627620290932,
3.12002238320872));
#98350=CARTESIAN_POINT('Ctrl Pts',(1.37840601855021,-0.198252265336022,
3.19949966605552));
#98351=CARTESIAN_POINT('Ctrl Pts',(0.912904206293459,1.0516239918919,3.27897694890232));
#98352=CARTESIAN_POINT('Ctrl Pts',(-0.389984008629303,1.33686932263319,
3.35845423174912));
#98353=CARTESIAN_POINT('Ctrl Pts',(-1.11101252964029,0.618991412974714,
3.41908428702707));
#98354=CARTESIAN_POINT('Ctrl Pts',(-1.17806221211803,0.11431017083026,3.45322191468942));
#98355=CARTESIAN_POINT('Ctrl Pts',(-1.17710658396666,0.00103751543904167,
3.46086711473616));
#98356=CARTESIAN_POINT('Origin',(0.,0.,0.612132885263843));
#98357=CARTESIAN_POINT('',(-1.17611517204452,0.000593537064731084,2.36213288526384));
#98358=CARTESIAN_POINT('',(-1.1770515199907,-0.00102726950455198,2.46086711473616));
#98359=CARTESIAN_POINT('',(-1.17775,-4.72972551152008E-14,0.612132885263843));
#98360=CARTESIAN_POINT('Ctrl Pts',(-1.17611517204452,0.000593537064731229,
2.36213288526384));
#98361=CARTESIAN_POINT('Ctrl Pts',(-1.17504706626748,-0.233952086459625,
2.37792963955861));
#98362=CARTESIAN_POINT('Ctrl Pts',(-0.993440962632586,-0.862822802044922,
2.42018164076696));
#98363=CARTESIAN_POINT('Ctrl Pts',(0.0307129365700887,-1.39159014732659,
2.48888888888889));
#98364=CARTESIAN_POINT('Ctrl Pts',(1.18564203741949,-0.729194359677473,
2.56825462962963));
#98365=CARTESIAN_POINT('Ctrl Pts',(1.25580231344031,0.600359775536952,2.64762037037037));
#98366=CARTESIAN_POINT('Ctrl Pts',(0.177001877056122,1.3806304142218,2.72698611111111));
#98367=CARTESIAN_POINT('Ctrl Pts',(-0.940839494469228,0.945566794997418,
2.79849028274227));
#98368=CARTESIAN_POINT('Ctrl Pts',(-1.17475785685998,0.274528336698561,
2.84353920745985));
#98369=CARTESIAN_POINT('Ctrl Pts',(-1.17701796998071,-0.00101206437339095,
2.86213288526384));
#98370=CARTESIAN_POINT('Ctrl Pts',(-1.1770515199907,-0.00102726950455214,
2.46086711473616));
#98371=CARTESIAN_POINT('Ctrl Pts',(-1.17801098215327,-0.116296063688412,
2.46864611663554));
#98372=CARTESIAN_POINT('Ctrl Pts',(-1.10947535590674,-0.623011746146892,
2.50291754615052));
#98373=CARTESIAN_POINT('Ctrl Pts',(-0.383235548912603,-1.33881925708758,
2.5636814032811));
#98374=CARTESIAN_POINT('Ctrl Pts',(0.918197143413365,-1.04700586255646,
2.6431586861279));
#98375=CARTESIAN_POINT('Ctrl Pts',(1.37738848098126,0.205202743845419,2.7226359689747));
#98376=CARTESIAN_POINT('Ctrl Pts',(0.573132410162518,1.26918330522814,2.80211325182151));
#98377=CARTESIAN_POINT('Ctrl Pts',(-0.755725509229907,1.16905515724181,
2.88152363374199));
#98378=CARTESIAN_POINT('Ctrl Pts',(-1.17960108716335,0.389288187712833,
2.93444158804687));
#98379=CARTESIAN_POINT('Ctrl Pts',(-1.17969113925438,-1.85122837469034E-5,
2.96086711473616));
#98380=CARTESIAN_POINT('Origin',(0.,0.,0.612132885263843));
#98381=CARTESIAN_POINT('',(-1.17916256915606,0.000764266613825465,1.86213288526384));
#98382=CARTESIAN_POINT('',(-1.17603208311293,0.000536542008743729,1.96086711473616));
#98383=CARTESIAN_POINT('',(-1.17775,-4.72972551152008E-14,0.612132885263843));
#98384=CARTESIAN_POINT('Ctrl Pts',(-1.17916256915606,0.000764266613825456,
1.86213288526384));
#98385=CARTESIAN_POINT('Ctrl Pts',(-1.1767421985046,-0.349243514957978,
1.8858648247438));
#98386=CARTESIAN_POINT('Ctrl Pts',(-0.826089096200879,-1.0939070674493,
1.93605201113733));
#98387=CARTESIAN_POINT('Ctrl Pts',(0.439473835276103,-1.32066405983435,
2.01269444444444));
#98388=CARTESIAN_POINT('Ctrl Pts',(1.34787702874157,-0.347428546246197,
2.09206018518518));
#98389=CARTESIAN_POINT('Ctrl Pts',(1.02310199861475,0.943810199691403,2.17142592592593));
#98390=CARTESIAN_POINT('Ctrl Pts',(-0.237743248735789,1.37146670874731,
2.25079166666666));
#98391=CARTESIAN_POINT('Ctrl Pts',(-1.07340543198276,0.708997793674441,
2.31436065311264));
#98392=CARTESIAN_POINT('Ctrl Pts',(-1.17683585157959,0.158847742356567,
2.35147439264503));
#98393=CARTESIAN_POINT('Ctrl Pts',(-1.17611517204452,0.000593537064731229,
2.36213288526384));
#98394=CARTESIAN_POINT('Ctrl Pts',(-1.17603208311293,0.000536542008743694,
1.96086711473616));
#98395=CARTESIAN_POINT('Ctrl Pts',(-1.17510603664511,-0.229512798367662,
1.9763582176086));
#98396=CARTESIAN_POINT('Ctrl Pts',(-0.998674096869405,-0.854308622825481,
2.01834174809664));
#98397=CARTESIAN_POINT('Ctrl Pts',(0.0166383981799684,-1.39248065884836,
2.08681770620029));
#98398=CARTESIAN_POINT('Ctrl Pts',(1.17979588449659,-0.739859513451799,
2.16629498904709));
#98399=CARTESIAN_POINT('Ctrl Pts',(1.2607599562499,0.591436597715745,2.24577227189389));
#98400=CARTESIAN_POINT('Ctrl Pts',(0.185253888314333,1.38021153969935,2.32524955474069));
#98401=CARTESIAN_POINT('Ctrl Pts',(-0.938280191320604,0.949667221313808,
2.39694783568812));
#98402=CARTESIAN_POINT('Ctrl Pts',(-1.17474340589855,0.276267175883094,
2.44215368901994));
#98403=CARTESIAN_POINT('Ctrl Pts',(-1.1770515199907,-0.00102726950455214,
2.46086711473616));
#98404=CARTESIAN_POINT('Origin',(0.,0.,5.75));
#98405=CARTESIAN_POINT('',(-1.40480161465946,0.000288650130247903,5.59314243068829));
#98406=CARTESIAN_POINT('Ctrl Pts',(0.200551794415766,1.1605490253568,5.82225));
#98407=CARTESIAN_POINT('Ctrl Pts',(0.250346736530993,1.15412464824318,5.82010127540114));
#98408=CARTESIAN_POINT('Ctrl Pts',(0.299515100252955,1.14429438809625,5.81796348399038));
#98409=CARTESIAN_POINT('Ctrl Pts',(0.347835451301076,1.13132131740438,5.81583221074506));
#98410=CARTESIAN_POINT('Ctrl Pts',(0.390115758468181,1.119969880549,5.81396734665541));
#98411=CARTESIAN_POINT('Ctrl Pts',(0.431747287002779,1.10621102058761,5.81210747303618));
#98412=CARTESIAN_POINT('Ctrl Pts',(0.472578058688195,1.09018611073377,5.81024963216711));
#98413=CARTESIAN_POINT('Ctrl Pts',(0.495740312305655,1.08109558878402,5.8091957265069));
#98414=CARTESIAN_POINT('Ctrl Pts',(0.518644777404426,1.07127528873862,5.8081424749863));
#98415=CARTESIAN_POINT('Ctrl Pts',(0.5412623142025,1.06074695780148,5.80708933767618));
#98416=CARTESIAN_POINT('Ctrl Pts',(0.551227651047345,1.05610815185461,5.80662532304307));
#98417=CARTESIAN_POINT('Ctrl Pts',(0.561129746489033,1.05133531419125,5.80616167994593));
#98418=CARTESIAN_POINT('Ctrl Pts',(0.570961984108289,1.04643304215269,5.80569856717539));
#98419=CARTESIAN_POINT('Ctrl Pts',(0.616614147837176,1.02367125237354,5.80354828350198));
#98420=CARTESIAN_POINT('Ctrl Pts',(0.660791536163919,0.998109158908003,
5.80140803169028));
#98421=CARTESIAN_POINT('Ctrl Pts',(0.703261793203859,0.969971780088759,
5.79927336313984));
#98422=CARTESIAN_POINT('Ctrl Pts',(0.746009532369701,0.941650563915182,
5.79712474759663));
#98423=CARTESIAN_POINT('Ctrl Pts',(0.787028757314936,0.910719705995268,
5.79498178851019));
#98424=CARTESIAN_POINT('Ctrl Pts',(0.826059377502829,0.877361822445158,
5.79283994951347));
#98425=CARTESIAN_POINT('Ctrl Pts',(0.833821521621903,0.87072783358265,5.79241399515014));
#98426=CARTESIAN_POINT('Ctrl Pts',(0.841506582511428,0.863996220736173,
5.79198799150201));
#98427=CARTESIAN_POINT('Ctrl Pts',(0.84910696954478,0.857173081813743,5.79156220485652));
#98428=CARTESIAN_POINT('Ctrl Pts',(0.887762460766018,0.822470666586745,
5.78939665830417));
#98429=CARTESIAN_POINT('Ctrl Pts',(0.924111480196861,0.785512508178675,
5.78724338870587));
#98430=CARTESIAN_POINT('Ctrl Pts',(0.957915058877359,0.74652009572043,5.78509790662306));
#98431=CARTESIAN_POINT('Ctrl Pts',(0.992826141795193,0.706250177633871,
5.78288213226379));
#98432=CARTESIAN_POINT('Ctrl Pts',(1.02502355391537,0.663810007535811,5.78067466406283));
#98433=CARTESIAN_POINT('Ctrl Pts',(1.05420839105705,0.619397315205114,5.77847055670522));
#98434=CARTESIAN_POINT('Ctrl Pts',(1.06880080962789,0.597190969039766,5.77736850302642));
#98435=CARTESIAN_POINT('Ctrl Pts',(1.08263941269998,0.574490831231967,5.77626728955846));
#98436=CARTESIAN_POINT('Ctrl Pts',(1.09568205036826,0.55131814869553,5.77516629813697));
#98437=CARTESIAN_POINT('Ctrl Pts',(1.10331783271695,0.537751754781692,5.77452172523108));
#98438=CARTESIAN_POINT('Ctrl Pts',(1.11068073284844,0.524023357137232,5.7738772284314));
#98439=CARTESIAN_POINT('Ctrl Pts',(1.11776167899029,0.510136920081813,5.77323268369607));
#98440=CARTESIAN_POINT('Ctrl Pts',(1.12229234159152,0.50125184176446,5.77282027910088));
#98441=CARTESIAN_POINT('Ctrl Pts',(1.12670826176501,0.492300592367051,5.7724077878105));
#98442=CARTESIAN_POINT('Ctrl Pts',(1.13100477448532,0.483288758243769,5.77199538723061));
#98443=CARTESIAN_POINT('Ctrl Pts',(1.13146311240594,0.482327405262425,5.77195139368595));
#98444=CARTESIAN_POINT('Ctrl Pts',(1.13192005003185,0.481365450766813,5.77190740518791));
#98445=CARTESIAN_POINT('Ctrl Pts',(1.13237558531186,0.480402896532057,5.77186342169889));
#98446=CARTESIAN_POINT('Ctrl Pts',(1.15347716745463,0.43581487417031,5.76982599178449));
#98447=CARTESIAN_POINT('Ctrl Pts',(1.17157311277187,0.389942668914696,5.76779931013149));
#98448=CARTESIAN_POINT('Ctrl Pts',(1.18676291197832,0.343097687180534,5.765779638305));
#98449=CARTESIAN_POINT('Ctrl Pts',(1.202674265336,0.294027449498257,5.76366402692258));
#98450=CARTESIAN_POINT('Ctrl Pts',(1.21539716018734,0.243888988733073,5.76155610715352));
#98451=CARTESIAN_POINT('Ctrl Pts',(1.22499689044219,0.193011403878154,5.75945158209943));
#98452=CARTESIAN_POINT('Ctrl Pts',(1.23231286325458,0.154237499020673,5.75784771952518));
#98453=CARTESIAN_POINT('Ctrl Pts',(1.23781388921226,0.11503357886763,5.7562458285991));
#98454=CARTESIAN_POINT('Ctrl Pts',(1.24150937798468,0.0755398256054352,
5.75464400739245));
#98455=CARTESIAN_POINT('Ctrl Pts',(1.24278142730073,0.0619454122763994,
5.75409263362411));
#98456=CARTESIAN_POINT('Ctrl Pts',(1.24383940039106,0.0483166402189457,
5.75354126811648));
#98457=CARTESIAN_POINT('Ctrl Pts',(1.24468321822901,0.034659203909744,5.75298983330018));
#98458=CARTESIAN_POINT('Ctrl Pts',(1.24534879298452,0.0238866835582429,
5.75255488030851));
#98459=CARTESIAN_POINT('Ctrl Pts',(1.24588107265531,0.0130945362466726,
5.75211981246084));
#98460=CARTESIAN_POINT('Ctrl Pts',(1.24627953946674,0.00230542954319881,
5.75168539011199));
#98461=CARTESIAN_POINT('Ctrl Pts',(1.24822972346125,-0.0504988256783816,
5.74955923182913));
#98462=CARTESIAN_POINT('Ctrl Pts',(1.24698640291456,-0.103332391097632,
5.74744435055885));
#98463=CARTESIAN_POINT('Ctrl Pts',(1.24262094207762,-0.155860577536359,
5.74533648797421));
#98464=CARTESIAN_POINT('Ctrl Pts',(1.23822829356669,-0.208715904513251,
5.74321549782232));
#98465=CARTESIAN_POINT('Ctrl Pts',(1.23067451535421,-0.261263213638418,
5.74110161405171));
#98466=CARTESIAN_POINT('Ctrl Pts',(1.21998110424804,-0.313168306918295,
5.73899049827755));
#98467=CARTESIAN_POINT('Ctrl Pts',(1.212546640722,-0.349254689361996,5.73752277080813));
#98468=CARTESIAN_POINT('Ctrl Pts',(1.20359355305155,-0.385030811129976,
5.73605638126527));
#98469=CARTESIAN_POINT('Ctrl Pts',(1.19311450906358,-0.420381654243896,
5.73458987174742));
#98470=CARTESIAN_POINT('Ctrl Pts',(1.18924384314627,-0.433439267490491,
5.73404818412643));
#98471=CARTESIAN_POINT('Ctrl Pts',(1.18516486509828,-0.446438816983626,
5.73350648013657));
#98472=CARTESIAN_POINT('Ctrl Pts',(1.18087679316331,-0.459374332873229,
5.73296468630611));
#98473=CARTESIAN_POINT('Ctrl Pts',(1.17751869200505,-0.469504473307045,
5.73254039340309));
#98474=CARTESIAN_POINT('Ctrl Pts',(1.17403481326548,-0.479587710603795,
5.73211636400189));
#98475=CARTESIAN_POINT('Ctrl Pts',(1.17042800339357,-0.48961426863002,5.73169286347098));
#98476=CARTESIAN_POINT('Ctrl Pts',(1.15233571380561,-0.539908960566405,
5.72956852242783));
#98477=CARTESIAN_POINT('Ctrl Pts',(1.13113574858936,-0.588834316433369,
5.72745512977291));
#98478=CARTESIAN_POINT('Ctrl Pts',(1.10685942649161,-0.636056546162735,
5.7253484324484));
#98479=CARTESIAN_POINT('Ctrl Pts',(1.09196285667379,-0.665033309582002,
5.72405570928987));
#98480=CARTESIAN_POINT('Ctrl Pts',(1.0759069315264,-0.693368745071741,5.72276550716582));
#98481=CARTESIAN_POINT('Ctrl Pts',(1.05868947708989,-0.720983087097389,
5.72147684339778));
#98482=CARTESIAN_POINT('Ctrl Pts',(1.0301474975545,-0.76676035271385,5.71934058016379));
#98483=CARTESIAN_POINT('Ctrl Pts',(0.998415979517414,-0.810558092677179,
5.71720854446415));
#98484=CARTESIAN_POINT('Ctrl Pts',(0.963808698514434,-0.852240620763262,
5.71507625961026));
#98485=CARTESIAN_POINT('Ctrl Pts',(0.955357655304655,-0.86241942810493,
5.71455555902606));
#98486=CARTESIAN_POINT('Ctrl Pts',(0.946734905694979,-0.872471932029711,
5.71403484358407));
#98487=CARTESIAN_POINT('Ctrl Pts',(0.937944627906372,-0.882395813911537,
5.71351404809364));
#98488=CARTESIAN_POINT('Ctrl Pts',(0.931659089334196,-0.889491942595295,
5.71314165028984));
#98489=CARTESIAN_POINT('Ctrl Pts',(0.925288554802937,-0.896521410431196,
5.71276925527006));
#98490=CARTESIAN_POINT('Ctrl Pts',(0.918843317495153,-0.90347434947744,
5.71239733132264));
#98491=CARTESIAN_POINT('Ctrl Pts',(0.882763429109284,-0.94239630886585,
5.71031533280649));
#98492=CARTESIAN_POINT('Ctrl Pts',(0.844277488058528,-0.979001068014847,
5.70824397827156));
#98493=CARTESIAN_POINT('Ctrl Pts',(0.803714874630552,-1.01319037638095,
5.70617927222703));
#98494=CARTESIAN_POINT('Ctrl Pts',(0.762328378480178,-1.04807411683791,
5.70407262915001));
#98495=CARTESIAN_POINT('Ctrl Pts',(0.718779165482597,-1.08044396964377,
5.7019729073863));
#98496=CARTESIAN_POINT('Ctrl Pts',(0.673373566240844,-1.11016225781405,
5.69987586300475));
#98497=CARTESIAN_POINT('Ctrl Pts',(0.647159389899234,-1.12731962297773,
5.69866516890243));
#98498=CARTESIAN_POINT('Ctrl Pts',(0.620325717407448,-1.14359251709036,
5.69745536720918));
#98499=CARTESIAN_POINT('Ctrl Pts',(0.59292679078264,-1.15894815486762,5.69624564125097));
#98500=CARTESIAN_POINT('Ctrl Pts',(0.573227863366542,-1.16998835356388,
5.69537588806061));
#98501=CARTESIAN_POINT('Ctrl Pts',(0.553236678223681,-1.18055431331316,
5.69450617401874));
#98502=CARTESIAN_POINT('Ctrl Pts',(0.532972640700167,-1.19063216004005,
5.69363619561337));
#98503=CARTESIAN_POINT('Ctrl Pts',(0.524118430766668,-1.19503559496727,
5.69325606547248));
#98504=CARTESIAN_POINT('Ctrl Pts',(0.515219619440634,-1.19934206145461,
5.69287620721068));
#98505=CARTESIAN_POINT('Ctrl Pts',(0.506281518471323,-1.20354925088432,
5.69249674135234));
#98506=CARTESIAN_POINT('Ctrl Pts',(0.456313640641153,-1.22706927243628,
5.69037536190998));
#98507=CARTESIAN_POINT('Ctrl Pts',(0.405086616979423,-1.2475067881456,5.68826478749503));
#98508=CARTESIAN_POINT('Ctrl Pts',(0.352918125008723,-1.26472873923489,
5.68616078779836));
#98509=CARTESIAN_POINT('Ctrl Pts',(0.301130796410408,-1.28182486002492,
5.68407216074501));
#98510=CARTESIAN_POINT('Ctrl Pts',(0.248414662726704,-1.29575277039046,
5.68199001268599));
#98511=CARTESIAN_POINT('Ctrl Pts',(0.195056298048485,-1.3063376162642,5.67991020536117));
#98512=CARTESIAN_POINT('Ctrl Pts',(0.157299308733902,-1.31382757430473,
5.67843850990324));
#98513=CARTESIAN_POINT('Ctrl Pts',(0.119220216467326,-1.3196427068114,5.67696798648358));
#98514=CARTESIAN_POINT('Ctrl Pts',(0.080917428897481,-1.3237050976022,5.67549716887144));
#98515=CARTESIAN_POINT('Ctrl Pts',(0.0675150714420637,-1.3251265506336,
5.67498252164494));
#98516=CARTESIAN_POINT('Ctrl Pts',(0.054085318460846,-1.32633328057544,
5.67446783839933));
#98517=CARTESIAN_POINT('Ctrl Pts',(0.0406323831126857,-1.32732152170149,
5.67395305632082));
#98518=CARTESIAN_POINT('Ctrl Pts',(0.0310947606857456,-1.32802214728863,
5.67358809529411));
#98519=CARTESIAN_POINT('Ctrl Pts',(0.0215549369531186,-1.3286122462768,
5.67322344616837));
#98520=CARTESIAN_POINT('Ctrl Pts',(0.0120155086475037,-1.32909103808168,
5.67285912622491));
#98521=CARTESIAN_POINT('Ctrl Pts',(-0.00344419505176427,-1.32986697341029,
5.67226870526915));
#98522=CARTESIAN_POINT('Ctrl Pts',(-0.0189037323976286,-1.33035065422119,
5.67167911528228));
#98523=CARTESIAN_POINT('Ctrl Pts',(-0.0343564581252633,-1.33053883536392,
5.67109026509666));
#98524=CARTESIAN_POINT('Ctrl Pts',(-0.0872006350171361,-1.33118236439367,
5.6690765554172));
#98525=CARTESIAN_POINT('Ctrl Pts',(-0.139964535350896,-1.32837422798037,
5.66707149739168));
#98526=CARTESIAN_POINT('Ctrl Pts',(-0.192401313336328,-1.32232893402684,
5.66507144501836));
#98527=CARTESIAN_POINT('Ctrl Pts',(-0.241586456950124,-1.31665851218333,
5.66319541702816));
#98528=CARTESIAN_POINT('Ctrl Pts',(-0.290484460932256,-1.30813920938173,
5.66132379313179));
#98529=CARTESIAN_POINT('Ctrl Pts',(-0.33889288810406,-1.29690893660877,
5.65945356440877));
#98530=CARTESIAN_POINT('Ctrl Pts',(-0.363232576035602,-1.29126237152394,
5.65851321608228));
#98531=CARTESIAN_POINT('Ctrl Pts',(-0.387448456924702,-1.28492988851642,
5.65757322046455));
#98532=CARTESIAN_POINT('Ctrl Pts',(-0.411514170147874,-1.277925756854,5.6566331950896));
#98533=CARTESIAN_POINT('Ctrl Pts',(-0.42593645895614,-1.27372826606078,
5.65606984933213));
#98534=CARTESIAN_POINT('Ctrl Pts',(-0.440304804608976,-1.26928951495865,
5.65550649288748));
#98535=CARTESIAN_POINT('Ctrl Pts',(-0.454613401700036,-1.26461222623906,
5.65494304343682));
#98536=CARTESIAN_POINT('Ctrl Pts',(-0.466630137166139,-1.26068411638425,
5.65446984379649));
#98537=CARTESIAN_POINT('Ctrl Pts',(-0.478607888322525,-1.25658647906165,
5.65399645163749));
#98538=CARTESIAN_POINT('Ctrl Pts',(-0.490518844838995,-1.25232993122734,
5.65352378741673));
#98539=CARTESIAN_POINT('Ctrl Pts',(-0.542976408693921,-1.23358348298773,
5.65144210627652));
#98540=CARTESIAN_POINT('Ctrl Pts',(-0.594232610756737,-1.21173023760249,
5.64937086575094));
#98541=CARTESIAN_POINT('Ctrl Pts',(-0.644015416885706,-1.186981761985,5.64730607728095));
#98542=CARTESIAN_POINT('Ctrl Pts',(-0.694431611488203,-1.1619184106019,
5.6452150184313));
#98543=CARTESIAN_POINT('Ctrl Pts',(-0.743337741202658,-1.13388527596091,
5.64313057686115));
#98544=CARTESIAN_POINT('Ctrl Pts',(-0.790438091635156,-1.10305083920001,
5.64104860982653));
#98545=CARTESIAN_POINT('Ctrl Pts',(-0.82903501505241,-1.07778320566126,
5.63934251801502));
#98546=CARTESIAN_POINT('Ctrl Pts',(-0.866419351609151,-1.05063337894,5.63763808789653));
#98547=CARTESIAN_POINT('Ctrl Pts',(-0.902414217563568,-1.02167191376899,
5.63593303979182));
#98548=CARTESIAN_POINT('Ctrl Pts',(-0.910920068938172,-1.01482810669252,
5.63553012439318));
#98549=CARTESIAN_POINT('Ctrl Pts',(-0.919348257804233,-1.00788305577541,
5.63512717448546));
#98550=CARTESIAN_POINT('Ctrl Pts',(-0.927696304763954,-1.00083754833469,
5.63472415998677));
#98551=CARTESIAN_POINT('Ctrl Pts',(-0.935430870222364,-0.994309801335792,
5.63435076222848));
#98552=CARTESIAN_POINT('Ctrl Pts',(-0.943089808691193,-0.987701554018673,
5.63397763797728));
#98553=CARTESIAN_POINT('Ctrl Pts',(-0.950669202156926,-0.981015938959458,
5.63360487756966));
#98554=CARTESIAN_POINT('Ctrl Pts',(-0.994716725700271,-0.942162594288292,
5.63143858644033));
#98555=CARTESIAN_POINT('Ctrl Pts',(-1.03610577124962,-0.900678804961991,
5.62928334127626));
#98556=CARTESIAN_POINT('Ctrl Pts',(-1.07451332611403,-0.856759471162354,
5.6271346426298));
#98557=CARTESIAN_POINT('Ctrl Pts',(-1.11097156084944,-0.815069199893007,
5.62509499808838));
#98558=CARTESIAN_POINT('Ctrl Pts',(-1.1447440267616,-0.771183458743441,
5.62306125240976));
#98559=CARTESIAN_POINT('Ctrl Pts',(-1.17552202326385,-0.725229965465032,
5.62102955705275));
#98560=CARTESIAN_POINT('Ctrl Pts',(-1.17716763689676,-0.722772960344077,
5.62092092796842));
#98561=CARTESIAN_POINT('Ctrl Pts',(-1.17880468047763,-0.720310036094466,
5.62081230474544));
#98562=CARTESIAN_POINT('Ctrl Pts',(-1.18043310341633,-0.717841209608489,
5.62070368679555));
#98563=CARTESIAN_POINT('Ctrl Pts',(-1.19779808226647,-0.691514437432329,
5.6195454198873));
#98564=CARTESIAN_POINT('Ctrl Pts',(-1.2141831700846,-0.664516719103805,
5.61838775260412));
#98565=CARTESIAN_POINT('Ctrl Pts',(-1.22958828555354,-0.636906248028152,
5.61722997163347));
#98566=CARTESIAN_POINT('Ctrl Pts',(-1.23690953438257,-0.623784429536166,
5.61667973865452));
#98567=CARTESIAN_POINT('Ctrl Pts',(-1.24400937600217,-0.610524175668424,
5.61612947999804));
#98568=CARTESIAN_POINT('Ctrl Pts',(-1.2508874161718,-0.597131552682936,
5.61557911909725));
#98569=CARTESIAN_POINT('Ctrl Pts',(-1.25640057861486,-0.58639656070315,
5.61513797176842));
#98570=CARTESIAN_POINT('Ctrl Pts',(-1.26177201580687,-0.575574540243382,
5.61469668149742));
#98571=CARTESIAN_POINT('Ctrl Pts',(-1.26699204746436,-0.564689109942556,
5.6142560315327));
#98572=CARTESIAN_POINT('Ctrl Pts',(-1.29112033611147,-0.514373935326777,
5.61221923745966));
#98573=CARTESIAN_POINT('Ctrl Pts',(-1.312066220014,-0.462614761951816,5.61019231073867));
#98574=CARTESIAN_POINT('Ctrl Pts',(-1.32987929292052,-0.409758600558678,
5.60817151787187));
#98575=CARTESIAN_POINT('Ctrl Pts',(-1.34804948442468,-0.355842772575017,
5.60611021191009));
#98576=CARTESIAN_POINT('Ctrl Pts',(-1.36296026011463,-0.300784543684916,
5.60405528821232));
#98577=CARTESIAN_POINT('Ctrl Pts',(-1.37461703271366,-0.244924160611515,
5.6020027842));
#98578=CARTESIAN_POINT('Ctrl Pts',(-1.38301163406865,-0.204696418030524,
5.60052467756142));
#98579=CARTESIAN_POINT('Ctrl Pts',(-1.38971768499473,-0.16405202684515,
5.59904782580349));
#98580=CARTESIAN_POINT('Ctrl Pts',(-1.39472131887101,-0.123113826832369,
5.59757074898948));
#98581=CARTESIAN_POINT('Ctrl Pts',(-1.39670759266725,-0.106862742927967,
5.59698439933976));
#98582=CARTESIAN_POINT('Ctrl Pts',(-1.39842544577593,-0.0905653426305087,
5.59639801422521));
#98583=CARTESIAN_POINT('Ctrl Pts',(-1.39987341132275,-0.0742292878849616,
5.59581150106865));
#98584=CARTESIAN_POINT('Ctrl Pts',(-1.40078997953924,-0.063888497252477,
5.59544023579991));
#98585=CARTESIAN_POINT('Ctrl Pts',(-1.40159832239367,-0.0535318605566342,
5.59506890679375));
#98586=CARTESIAN_POINT('Ctrl Pts',(-1.40229726272754,-0.0431766457076119,
5.59469803805592));
#98587=CARTESIAN_POINT('Ctrl Pts',(-1.40327566417533,-0.0286810490031125,
5.59417888285419));
#98588=CARTESIAN_POINT('Ctrl Pts',(-1.40404039706439,-0.0141809540206952,
5.5936603676618));
#98589=CARTESIAN_POINT('Ctrl Pts',(-1.40459200171434,0.000318079185916144,
5.59314243068829));
#98590=CARTESIAN_POINT('',(0.632686155053592,1.31670003839153,5.5365));
#98591=CARTESIAN_POINT('Ctrl Pts',(0.632684721053846,1.31669749784948,5.5365));
#98592=CARTESIAN_POINT('Ctrl Pts',(0.5776126161197,1.33489715577749,5.5438663413747));
#98593=CARTESIAN_POINT('Ctrl Pts',(0.521701465845253,1.34991581051279,5.5512639488319));
#98594=CARTESIAN_POINT('Ctrl Pts',(0.465251304334383,1.36164744646314,5.55870934620359));
#98595=CARTESIAN_POINT('Ctrl Pts',(0.410290964957589,1.37306946326556,5.56595824603648));
#98596=CARTESIAN_POINT('Ctrl Pts',(0.354818674551029,1.38137556945319,5.57325244654584));
#98597=CARTESIAN_POINT('Ctrl Pts',(0.299116808798334,1.38641968110749,5.58060719750617));
#98598=CARTESIAN_POINT('Ctrl Pts',(0.265773215134626,1.3894391277117,5.58500981174906));
#98599=CARTESIAN_POINT('Ctrl Pts',(0.232347534925492,1.39128877703379,5.58943412314275));
#98600=CARTESIAN_POINT('Ctrl Pts',(0.198903503703726,1.39192889738093,5.59388340276906));
#98601=CARTESIAN_POINT('Ctrl Pts',(0.174835521717936,1.39238955970006,5.59708532484554));
#98602=CARTESIAN_POINT('Ctrl Pts',(0.150758086854015,1.39222368124497,5.60030017785668));
#98603=CARTESIAN_POINT('Ctrl Pts',(0.126696106755384,1.39141440232077,5.60352918094528));
#98604=CARTESIAN_POINT('Ctrl Pts',(0.116740991131968,1.39107958094576,5.6048651100319));
#98605=CARTESIAN_POINT('Ctrl Pts',(0.106789185635262,1.39063453208846,5.6062033764661));
#98606=CARTESIAN_POINT('Ctrl Pts',(0.096855542906272,1.39007904004502,5.60754230086134));
#98607=CARTESIAN_POINT('Ctrl Pts',(0.0431629060528989,1.38707653297111,
5.61477936215785));
#98608=CARTESIAN_POINT('Ctrl Pts',(-0.0101013612254671,1.38084853180898,
5.62204918559313));
#98609=CARTESIAN_POINT('Ctrl Pts',(-0.062681467909731,1.37127180372221,
5.62936778152763));
#98610=CARTESIAN_POINT('Ctrl Pts',(-0.0748777648155605,1.3690504195049,
5.63106537734056));
#98611=CARTESIAN_POINT('Ctrl Pts',(-0.0870371762268703,1.36664865395529,
5.6327655972999));
#98612=CARTESIAN_POINT('Ctrl Pts',(-0.0991563532317366,1.36406459322577,
5.63446864121724));
#98613=CARTESIAN_POINT('Ctrl Pts',(-0.151155968387667,1.3529771931968,5.64177587241452));
#98614=CARTESIAN_POINT('Ctrl Pts',(-0.20241723694028,1.33853649093085,5.64913509270409));
#98615=CARTESIAN_POINT('Ctrl Pts',(-0.252697184270726,1.32091854822008,
5.65656208552686));
#98616=CARTESIAN_POINT('Ctrl Pts',(-0.276692007497009,1.31251083414319,
5.66010642853729));
#98617=CARTESIAN_POINT('Ctrl Pts',(-0.300462900284357,1.30337900742421,
5.66366620628353));
#98618=CARTESIAN_POINT('Ctrl Pts',(-0.323980669253028,1.29353978580801,
5.66724313418339));
#98619=CARTESIAN_POINT('Ctrl Pts',(-0.344366643764626,1.28501082537181,
5.67034373276029));
#98620=CARTESIAN_POINT('Ctrl Pts',(-0.364562398637558,1.27595029836785,
5.67345721794848));
#98621=CARTESIAN_POINT('Ctrl Pts',(-0.384547613705539,1.26636838485261,
5.67658470706387));
#98622=CARTESIAN_POINT('Ctrl Pts',(-0.393231305074717,1.26220498809107,
5.67794361914694));
#98623=CARTESIAN_POINT('Ctrl Pts',(-0.401871759831675,1.2579447372934,5.67930463795576));
#98624=CARTESIAN_POINT('Ctrl Pts',(-0.410459095485719,1.25359307181017,
5.68066652441999));
#98625=CARTESIAN_POINT('Ctrl Pts',(-0.457860218704337,1.22957236968709,
5.68818398393266));
#98626=CARTESIAN_POINT('Ctrl Pts',(-0.503723345675591,1.20273254085136,
5.69574001132433));
#98627=CARTESIAN_POINT('Ctrl Pts',(-0.547817782657036,1.17327249559497,
5.70335294833422));
#98628=CARTESIAN_POINT('Ctrl Pts',(-0.591573456579066,1.14403878217871,
5.71090739765249));
#98629=CARTESIAN_POINT('Ctrl Pts',(-0.633588209819031,1.11222397120681,
5.71851788551221));
#98630=CARTESIAN_POINT('Ctrl Pts',(-0.67359559348855,1.07799259910652,5.7262023341514));
#98631=CARTESIAN_POINT('Ctrl Pts',(-0.695111525426927,1.05958300055963,
5.73033502313878));
#98632=CARTESIAN_POINT('Ctrl Pts',(-0.716046101869675,1.04047404160734,
5.73448910363906));
#98633=CARTESIAN_POINT('Ctrl Pts',(-0.736351872882751,1.02068919616837,
5.7386673633923));
#98634=CARTESIAN_POINT('Ctrl Pts',(-0.751657458360816,1.00577626117853,
5.74181674943439));
#98635=CARTESIAN_POINT('Ctrl Pts',(-0.766605704164082,0.990479292062633,
5.74497987285309));
#98636=CARTESIAN_POINT('Ctrl Pts',(-0.781174508355632,0.974808057976537,
5.7481579274816));
#98637=CARTESIAN_POINT('Ctrl Pts',(-0.787955137137737,0.967514335067083,
5.74963706114294));
#98638=CARTESIAN_POINT('Ctrl Pts',(-0.794654129011777,0.960138725612505,
5.75111957954705));
#98639=CARTESIAN_POINT('Ctrl Pts',(-0.801258369521843,0.952694819900035,
5.75260312372203));
#98640=CARTESIAN_POINT('Ctrl Pts',(-0.83461777006059,0.915094094751325,
5.76009681573319));
#98641=CARTESIAN_POINT('Ctrl Pts',(-0.865631920666325,0.875680189096366,
5.76763145065592));
#98642=CARTESIAN_POINT('Ctrl Pts',(-0.894075852218896,0.834608475514328,
5.77522568029987));
#98643=CARTESIAN_POINT('Ctrl Pts',(-0.922876152304258,0.793022182353815,
5.78291505658242));
#98644=CARTESIAN_POINT('Ctrl Pts',(-0.949042126947202,0.749735397248123,
5.79066553024238));
#98645=CARTESIAN_POINT('Ctrl Pts',(-0.972286221838532,0.704896061770876,
5.79849646296423));
#98646=CARTESIAN_POINT('Ctrl Pts',(-0.994114901027574,0.662787153088537,
5.80585054230935));
#98647=CARTESIAN_POINT('Ctrl Pts',(-1.01336659524672,0.619308291408811,
5.81327558018311));
#98648=CARTESIAN_POINT('Ctrl Pts',(-1.02975283339989,0.574581994853113,
5.82078761227338));
#98649=CARTESIAN_POINT('Ctrl Pts',(-1.03081535021928,0.57168185133541,5.82127470762554));
#98650=CARTESIAN_POINT('Ctrl Pts',(-1.03186580105051,0.568776465116369,
5.82176216874382));
#98651=CARTESIAN_POINT('Ctrl Pts',(-1.03290409957988,0.565865870654058,
5.82225));
#98652=CARTESIAN_POINT('',(-0.632402293996042,1.31836377294842,5.53649999999999));
#98653=CARTESIAN_POINT('Origin',(0.,0.,5.5365));
#98654=CARTESIAN_POINT('Ctrl Pts',(-1.40459200171434,0.000318079185916144,
5.59314243068829));
#98655=CARTESIAN_POINT('Ctrl Pts',(-1.40680778098466,0.0585602590185899,
5.59106189346052));
#98656=CARTESIAN_POINT('Ctrl Pts',(-1.4055885051658,0.116784323458512,5.58899068555129));
#98657=CARTESIAN_POINT('Ctrl Pts',(-1.40093750525803,0.174640198144212,
5.58692480237197));
#98658=CARTESIAN_POINT('Ctrl Pts',(-1.39633232148189,0.231926145411667,
5.58487926982209));
#98659=CARTESIAN_POINT('Ctrl Pts',(-1.38836273052522,0.28885226195592,5.58283895761298));
#98660=CARTESIAN_POINT('Ctrl Pts',(-1.37698165172494,0.345081547364195,
5.58079997833938));
#98661=CARTESIAN_POINT('Ctrl Pts',(-1.37163519174172,0.371496233493362,
5.57984213231404));
#98662=CARTESIAN_POINT('Ctrl Pts',(-1.36553515098603,0.397757077520593,
5.57888458044281));
#98663=CARTESIAN_POINT('Ctrl Pts',(-1.35867270637224,0.423828272539498,
5.5779269197225));
#98664=CARTESIAN_POINT('Ctrl Pts',(-1.3550589480402,0.437557344834855,5.57742261628516));
#98665=CARTESIAN_POINT('Ctrl Pts',(-1.35123372725876,0.451233812302909,
5.57691828266322));
#98666=CARTESIAN_POINT('Ctrl Pts',(-1.34719546760397,0.464852331742502,
5.57641386000633));
#98667=CARTESIAN_POINT('Ctrl Pts',(-1.34347158307698,0.477410660863661,
5.57594870623028));
#98668=CARTESIAN_POINT('Ctrl Pts',(-1.33956525510877,0.489923136969561,
5.57548334714617));
#98669=CARTESIAN_POINT('Ctrl Pts',(-1.33548376997894,0.502360503152716,
5.5750186753579));
#98670=CARTESIAN_POINT('Ctrl Pts',(-1.32167213509367,0.544448212697522,
5.57344623864017));
#98671=CARTESIAN_POINT('Ctrl Pts',(-1.30584082143809,0.585731598763993,
5.57187962186733));
#98672=CARTESIAN_POINT('Ctrl Pts',(-1.2879823448929,0.626060508418404,5.57031710849444));
#98673=CARTESIAN_POINT('Ctrl Pts',(-1.26509212904047,0.677752344771133,
5.56831434704458));
#98674=CARTESIAN_POINT('Ctrl Pts',(-1.23887339227609,0.727877279493874,
5.56631832706785));
#98675=CARTESIAN_POINT('Ctrl Pts',(-1.20962767910274,0.776285009599572,
5.56432543386955));
#98676=CARTESIAN_POINT('Ctrl Pts',(-1.17972369750887,0.825782310674114,
5.56228768422853));
#98677=CARTESIAN_POINT('Ctrl Pts',(-1.14665431471445,0.873484996740448,
5.56025320370633));
#98678=CARTESIAN_POINT('Ctrl Pts',(-1.11069355490779,0.919207501903464,
5.55821812799238));
#98679=CARTESIAN_POINT('Ctrl Pts',(-1.10074051269562,0.931862351978381,
5.55765486974659));
#98680=CARTESIAN_POINT('Ctrl Pts',(-1.0905657304381,0.944365329077774,5.55709156590646));
#98681=CARTESIAN_POINT('Ctrl Pts',(-1.08017448707633,0.956712047355874,
5.55652813454011));
#98682=CARTESIAN_POINT('Ctrl Pts',(-1.07336013054068,0.964808762778951,
5.55615864822553));
#98683=CARTESIAN_POINT('Ctrl Pts',(-1.06645228235592,0.972838575185135,
5.55578909024319));
#98684=CARTESIAN_POINT('Ctrl Pts',(-1.05946296377322,0.980788625511553,
5.55541998337116));
#98685=CARTESIAN_POINT('Ctrl Pts',(-1.0207932618269,1.0247737540964,5.55337783111282));
#98686=CARTESIAN_POINT('Ctrl Pts',(-0.979560085515444,1.06640812044688,
5.55134545805107));
#98687=CARTESIAN_POINT('Ctrl Pts',(-0.936079694160814,1.10553268147045,
5.54931910582972));
#98688=CARTESIAN_POINT('Ctrl Pts',(-0.890073531427023,1.14692998414553,
5.54717504302009));
#98689=CARTESIAN_POINT('Ctrl Pts',(-0.841550919085985,1.185518576841,5.54503772086778));
#98690=CARTESIAN_POINT('Ctrl Pts',(-0.790836296596859,1.22107346264117,
5.54290268726531));
#98691=CARTESIAN_POINT('Ctrl Pts',(-0.740121674107733,1.25662834844134,
5.54076765366285));
#98692=CARTESIAN_POINT('Ctrl Pts',(-0.68721393539805,1.2891504552414,5.53863490861023));
#98693=CARTESIAN_POINT('Ctrl Pts',(-0.632402293996098,1.31836377294839,
5.5365));
#98694=CARTESIAN_POINT('',(-0.999999999999998,-1.22464679914735E-16,6.));
#98695=CARTESIAN_POINT('',(-1.25,-1.53080849893419E-16,5.75));
#98696=CARTESIAN_POINT('Origin',(0.,0.,6.));
#98697=CARTESIAN_POINT('Ctrl Pts',(0.850780204044567,-1.1908002747757,1.37152216057906));
#98698=CARTESIAN_POINT('Ctrl Pts',(1.24665751306111,-0.907961426921765,
1.39797740749264));
#98699=CARTESIAN_POINT('Ctrl Pts',(1.72735056947482,0.0786343709257417,
1.4508879013198));
#98700=CARTESIAN_POINT('Ctrl Pts',(0.869444322178829,1.49656652414857,1.53025364206055));
#98701=CARTESIAN_POINT('Ctrl Pts',(-0.784660621780123,1.54085420010821,
1.60961938280129));
#98702=CARTESIAN_POINT('Ctrl Pts',(-1.72048121864664,0.177590566749858,
1.68898512354203));
#98703=CARTESIAN_POINT('Ctrl Pts',(-1.08239711820243,-1.34930263152836,
1.76835086428277));
#98704=CARTESIAN_POINT('Ctrl Pts',(0.546100579856982,-1.64108839020809,
1.84771660502351));
#98705=CARTESIAN_POINT('Ctrl Pts',(1.67490386887139,-0.431722927133368,
1.92708234576425));
#98706=CARTESIAN_POINT('Ctrl Pts',(1.27133073655079,1.17280087221257,2.00644808650499));
#98707=CARTESIAN_POINT('Ctrl Pts',(-0.295425382742359,1.7042169630666,2.08581382724573));
#98708=CARTESIAN_POINT('Ctrl Pts',(-1.59188248145604,0.676454136362828,
2.16517956798647));
#98709=CARTESIAN_POINT('Ctrl Pts',(-1.43189637910881,-0.970235084489994,
2.24454530872721));
#98710=CARTESIAN_POINT('Ctrl Pts',(0.0381646212441605,-1.72922282369982,
2.32391104946795));
#98711=CARTESIAN_POINT('Ctrl Pts',(1.47330683231875,-0.906114154436845,
2.40327679020869));
#98712=CARTESIAN_POINT('Ctrl Pts',(1.56048965036714,0.746021253660212,2.48264253094943));
#98713=CARTESIAN_POINT('Ctrl Pts',(0.219946717955126,1.71560400018136,2.56200827169018));
#98714=CARTESIAN_POINT('Ctrl Pts',(-1.32183001348916,1.11554483087117,2.64137401243091));
#98715=CARTESIAN_POINT('Ctrl Pts',(-1.6542362198257,-0.505150719675214,
2.72073975317166));
#98716=CARTESIAN_POINT('Ctrl Pts',(-0.47314620318653,-1.66367278437318,
2.80010549391239));
#98717=CARTESIAN_POINT('Ctrl Pts',(1.14083539250324,-1.30006509600873,2.87947123465314));
#98718=CARTESIAN_POINT('Ctrl Pts',(1.71104224612908,0.253000088961462,2.95883697539387));
#98719=CARTESIAN_POINT('Ctrl Pts',(0.715779865238755,1.57459003111278,3.03820271613462));
#98720=CARTESIAN_POINT('Ctrl Pts',(-0.934364853836859,1.45555382197998,
3.11756845687536));
#98721=CARTESIAN_POINT('Ctrl Pts',(-1.72963914154473,0.00480021022192471,
3.1969341976161));
#98722=CARTESIAN_POINT('Ctrl Pts',(-0.942429502195046,-1.45034521121045,
3.27629993835684));
#98723=CARTESIAN_POINT('Ctrl Pts',(0.707029089469739,-1.57853871314733,
3.35566567909759));
#98724=CARTESIAN_POINT('Ctrl Pts',(1.70961161212856,-0.262493308300521,
3.43503141983832));
#98725=CARTESIAN_POINT('Ctrl Pts',(1.14803382433629,1.29371285008445,3.51439716057907));
#98726=CARTESIAN_POINT('Ctrl Pts',(-0.463904717388525,1.66627339125727,
3.5937629013198));
#98727=CARTESIAN_POINT('Ctrl Pts',(-1.65140689002388,0.514324689124398,
3.67312864206055));
#98728=CARTESIAN_POINT('Ctrl Pts',(-1.32800149895114,-1.10819069526513,
3.75249438280128));
#98729=CARTESIAN_POINT('Ctrl Pts',(0.210420926876642,-1.71679865899124,
3.83186012354203));
#98730=CARTESIAN_POINT('Ctrl Pts',(1.55632474164788,-0.754670727735459,
3.91122586428277));
#98731=CARTESIAN_POINT('Ctrl Pts',(1.47831367962429,0.897921625865326,3.99059160502351));
#98732=CARTESIAN_POINT('Ctrl Pts',(0.0477617634505684,1.72898624257253,
4.06995734576425));
#98733=CARTESIAN_POINT('Ctrl Pts',(-1.42648845110344,0.97816427327762,4.14932308650499));
#98734=CARTESIAN_POINT('Ctrl Pts',(-1.59561373357911,-0.667601135609854,
4.22868882724573));
#98735=CARTESIAN_POINT('Ctrl Pts',(-0.30487794355985,-1.70256399589041,
4.30805456798647));
#98736=CARTESIAN_POINT('Ctrl Pts',(1.26479746913964,-1.17981448384994,4.38742030872722));
#98737=CARTESIAN_POINT('Ctrl Pts',(1.67728207661725,0.422372441852027,4.46678604946795));
#98738=CARTESIAN_POINT('Ctrl Pts',(0.555186290818104,1.63812204743828,4.54615179020869));
#98739=CARTESIAN_POINT('Ctrl Pts',(-1.07486310747744,1.35511814363614,4.62551753094944));
#98740=CARTESIAN_POINT('Ctrl Pts',(-1.72149382964358,-0.167711379513054,
4.70488327169017));
#98741=CARTESIAN_POINT('Ctrl Pts',(-0.793099380882797,-1.53710010465276,
4.78424901243091));
#98742=CARTESIAN_POINT('Ctrl Pts',(0.860930945424167,-1.50015930506732,
4.86361475317166));
#98743=CARTESIAN_POINT('Ctrl Pts',(1.72725376076341,-0.0906976289718168,
4.9429804939124));
#98744=CARTESIAN_POINT('Ctrl Pts',(1.01331952241407,1.4017586358057,5.02234623465314));
#98745=CARTESIAN_POINT('Ctrl Pts',(-0.627807088834987,1.61169039054698,
5.10171197539388));
#98746=CARTESIAN_POINT('Ctrl Pts',(-1.69437838885534,0.347100595182272,
5.18107771613462));
#98747=CARTESIAN_POINT('Ctrl Pts',(-1.2110334922522,-1.23515140512641,5.26044345687535));
#98748=CARTESIAN_POINT('Ctrl Pts',(0.38089666041727,-1.68716085990558,5.33980919761611));
#98749=CARTESIAN_POINT('Ctrl Pts',(1.6232201233188,-0.59588622120029,5.41917493835683));
#98750=CARTESIAN_POINT('Ctrl Pts',(1.38257289293014,1.0412189905615,5.49854067909759));
#98751=CARTESIAN_POINT('Ctrl Pts',(-0.127306102888356,1.72444672585826,
5.57790641983832));
#98752=CARTESIAN_POINT('Ctrl Pts',(-1.04974858331048,1.12985699072368,5.63081691366548));
#98753=CARTESIAN_POINT('Ctrl Pts',(-1.28351105899822,0.703158311782828,
5.65727216057906));
#98754=CARTESIAN_POINT('Ctrl Pts',(0.795408277542864,-1.11329858282327,
1.42651477371938));
#98755=CARTESIAN_POINT('Ctrl Pts',(1.16552042517654,-0.848867934667374,
1.45297002063296));
#98756=CARTESIAN_POINT('Ctrl Pts',(1.61492819725584,0.0735165548473875,
1.50588051446012));
#98757=CARTESIAN_POINT('Ctrl Pts',(0.812857665747304,1.39916443229674,1.58524625520086));
#98758=CARTESIAN_POINT('Ctrl Pts',(-0.733592002562801,1.4405697022877,1.6646119959416));
#98759=CARTESIAN_POINT('Ctrl Pts',(-1.60850592921986,0.166032314967876,
1.74397773668234));
#98760=CARTESIAN_POINT('Ctrl Pts',(-1.01195070514552,-1.26148501919281,
1.82334347742308));
#98761=CARTESIAN_POINT('Ctrl Pts',(0.510558331663356,-1.53428028008351,
1.90270921816382));
#98762=CARTESIAN_POINT('Ctrl Pts',(1.56589492216145,-0.403624800170977,
1.98207495890456));
#98763=CARTESIAN_POINT('Ctrl Pts',(1.18858782390544,1.09647064803885,2.0614406996453));
#98764=CARTESIAN_POINT('Ctrl Pts',(-0.27619800474017,1.59330021162684,2.14080644038604));
#98765=CARTESIAN_POINT('Ctrl Pts',(-1.4882768741047,0.632427995953832,2.22017218112678));
#98766=CARTESIAN_POINT('Ctrl Pts',(-1.33870325979885,-0.907088591973651,
2.29953792186753));
#98767=CARTESIAN_POINT('Ctrl Pts',(0.0356807263528025,-1.61667859824208,
2.37890366260826));
#98768=CARTESIAN_POINT('Ctrl Pts',(1.37741856735233,-0.847140889517054,
2.45826940334901));
#98769=CARTESIAN_POINT('Ctrl Pts',(1.45892720472486,0.697467427619125,2.53763514408974));
#98770=CARTESIAN_POINT('Ctrl Pts',(0.205631770988793,1.60394613819484,2.61700088483048));
#98771=CARTESIAN_POINT('Ctrl Pts',(-1.23580042087909,1.04294104191286,2.69636662557123));
#98772=CARTESIAN_POINT('Ctrl Pts',(-1.54657240025727,-0.472273640038004,
2.77573236631196));
#98773=CARTESIAN_POINT('Ctrl Pts',(-0.442352096009542,-1.55539479823614,
2.85509810705271));
#98774=CARTESIAN_POINT('Ctrl Pts',(1.06658560013157,-1.21545204483358,2.93446384779345));
#98775=CARTESIAN_POINT('Ctrl Pts',(1.59968127999051,0.236533906198515,3.01382958853419));
#98776=CARTESIAN_POINT('Ctrl Pts',(0.669194260753619,1.47210988047151,3.09319532927493));
#98777=CARTESIAN_POINT('Ctrl Pts',(-0.873552928775051,1.3608209886738,3.17256107001567));
#98778=CARTESIAN_POINT('Ctrl Pts',(-1.61706782057982,0.0044877947633364,
3.25192681075641));
#98779=CARTESIAN_POINT('Ctrl Pts',(-0.881092699951054,-1.35595137358299,
3.33129255149715));
#98780=CARTESIAN_POINT('Ctrl Pts',(0.661013017879724,-1.47580156765551,
3.41065829223789));
#98781=CARTESIAN_POINT('Ctrl Pts',(1.59834375694903,-0.245409271665311,
3.49002403297863));
#98782=CARTESIAN_POINT('Ctrl Pts',(1.07331553136189,1.20951322659928,3.56938977371938));
#98783=CARTESIAN_POINT('Ctrl Pts',(-0.433712080332666,1.557826147993,3.64875551446012));
#98784=CARTESIAN_POINT('Ctrl Pts',(-1.54392721371723,0.480850533580084,
3.72812125520086));
#98785=CARTESIAN_POINT('Ctrl Pts',(-1.24157024321141,-1.03606554068775,
3.80748699594159));
#98786=CARTESIAN_POINT('Ctrl Pts',(0.196725953671999,-1.60506304418501,
3.88685273668234));
#98787=CARTESIAN_POINT('Ctrl Pts',(1.45503336368959,-0.705553961888648,
3.96621847742308));
#98788=CARTESIAN_POINT('Ctrl Pts',(1.38209955049261,0.839481561045601,4.04558421816382));
#98789=CARTESIAN_POINT('Ctrl Pts',(0.044653251001868,1.61645741469071,4.12494995890456));
#98790=CARTESIAN_POINT('Ctrl Pts',(-1.33364729977607,0.914501719789614,
4.20431569964529));
#98791=CARTESIAN_POINT('Ctrl Pts',(-1.49176528252109,-0.624151181276522,
4.28368144038605));
#98792=CARTESIAN_POINT('Ctrl Pts',(-0.285035357892558,-1.59175482567615,
4.36304718112678));
#98793=CARTESIAN_POINT('Ctrl Pts',(1.18247976573305,-1.10302778785629,4.44241292186753));
#98794=CARTESIAN_POINT('Ctrl Pts',(1.56811834733964,0.394882879100816,4.52177866260826));
#98795=CARTESIAN_POINT('Ctrl Pts',(0.519052710906638,1.53150699788686,4.601144403349));
#98796=CARTESIAN_POINT('Ctrl Pts',(-1.00490703574035,1.26692203623515,4.68051014408975));
#98797=CARTESIAN_POINT('Ctrl Pts',(-1.60945263574296,-0.156796101823534,
4.75987588483049));
#98798=CARTESIAN_POINT('Ctrl Pts',(-0.741481535970538,-1.43705993726761,
4.83924162557122));
#98799=CARTESIAN_POINT('Ctrl Pts',(0.804898371080712,-1.40252338172761,
4.91860736631197));
#98800=CARTESIAN_POINT('Ctrl Pts',(1.61483768921389,-0.0847946913841371,
4.99797310705271));
#98801=CARTESIAN_POINT('Ctrl Pts',(0.94736893511653,1.31052699244357,5.07733884779345));
#98802=CARTESIAN_POINT('Ctrl Pts',(-0.58694707844105,1.50679561111438,5.15670458853418));
#98803=CARTESIAN_POINT('Ctrl Pts',(-1.58410196826192,0.324510002977889,
5.23607032927493));
#98804=CARTESIAN_POINT('Ctrl Pts',(-1.13221494757367,-1.15476317735853,
5.31543607001568));
#98805=CARTESIAN_POINT('Ctrl Pts',(0.356106495125341,-1.57735418282597,
5.3948018107564));
#98806=CARTESIAN_POINT('Ctrl Pts',(1.51757494617763,-0.55710373908937,5.47416755149716));
#98807=CARTESIAN_POINT('Ctrl Pts',(1.29258992876779,0.97345260255263,5.55353329223789));
#98808=CARTESIAN_POINT('Ctrl Pts',(-0.119020550240519,1.61221334653609,
5.63289903297864));
#98809=CARTESIAN_POINT('Ctrl Pts',(-0.981427057816582,1.05632171339779,
5.6858095268058));
#98810=CARTESIAN_POINT('Ctrl Pts',(-1.19997540585877,0.657394164739904,
5.71226477371938));
#98811=CARTESIAN_POINT('Ctrl Pts',(0.740036351041162,-1.03579689087083,
1.48150738685969));
#98812=CARTESIAN_POINT('Ctrl Pts',(1.08438333729197,-0.789774442412982,
1.50796263377327));
#98813=CARTESIAN_POINT('Ctrl Pts',(1.50250582503687,0.0683987387690329,
1.56087312760043));
#98814=CARTESIAN_POINT('Ctrl Pts',(0.756271009315778,1.30176234044491,1.64023886834117));
#98815=CARTESIAN_POINT('Ctrl Pts',(-0.682523383345477,1.3402852044672,1.71960460908191));
#98816=CARTESIAN_POINT('Ctrl Pts',(-1.49653063979308,0.154474063185896,
1.79897034982265));
#98817=CARTESIAN_POINT('Ctrl Pts',(-0.941504292088612,-1.17366740685727,
1.87833609056339));
#98818=CARTESIAN_POINT('Ctrl Pts',(0.475016083469731,-1.42747216995893,
1.95770183130413));
#98819=CARTESIAN_POINT('Ctrl Pts',(1.45688597545151,-0.375526673208587,
2.03706757204487));
#98820=CARTESIAN_POINT('Ctrl Pts',(1.1058449112601,1.02014042386513,2.11643331278562));
#98821=CARTESIAN_POINT('Ctrl Pts',(-0.25697062673798,1.48238346018707,2.19579905352635));
#98822=CARTESIAN_POINT('Ctrl Pts',(-1.38467126675336,0.588401855544837,
2.2751647942671));
#98823=CARTESIAN_POINT('Ctrl Pts',(-1.2455101404889,-0.843942099457309,
2.35453053500783));
#98824=CARTESIAN_POINT('Ctrl Pts',(0.0331968314614454,-1.50413437278434,
2.43389627574858));
#98825=CARTESIAN_POINT('Ctrl Pts',(1.28153030238591,-0.788167624597264,
2.51326201648932));
#98826=CARTESIAN_POINT('Ctrl Pts',(1.35736475908259,0.648913601578039,2.59262775723006));
#98827=CARTESIAN_POINT('Ctrl Pts',(0.191316824022457,1.49228827620832,2.6719934979708));
#98828=CARTESIAN_POINT('Ctrl Pts',(-1.14977082826902,0.970337252954552,
2.75135923871154));
#98829=CARTESIAN_POINT('Ctrl Pts',(-1.43890858068883,-0.439396560400792,
2.83072497945228));
#98830=CARTESIAN_POINT('Ctrl Pts',(-0.411557988832554,-1.44711681209911,
2.91009072019302));
#98831=CARTESIAN_POINT('Ctrl Pts',(0.992335807759912,-1.13083899365843,
2.98945646093376));
#98832=CARTESIAN_POINT('Ctrl Pts',(1.48832031385195,0.220067723435567,3.0688222016745));
#98833=CARTESIAN_POINT('Ctrl Pts',(0.622608656268483,1.36962972983025,3.14818794241524));
#98834=CARTESIAN_POINT('Ctrl Pts',(-0.812741003713242,1.26608815536762,
3.22755368315598));
#98835=CARTESIAN_POINT('Ctrl Pts',(-1.50449649961492,0.00417537930474892,
3.30691942389672));
#98836=CARTESIAN_POINT('Ctrl Pts',(-0.819755897707061,-1.26155753595553,
3.38628516463747));
#98837=CARTESIAN_POINT('Ctrl Pts',(0.614996946289707,-1.37306442216368,
3.4656509053782));
#98838=CARTESIAN_POINT('Ctrl Pts',(1.4870759017695,-0.2283252350301,3.54501664611895));
#98839=CARTESIAN_POINT('Ctrl Pts',(0.998597238387491,1.12531360311411,3.62438238685968));
#98840=CARTESIAN_POINT('Ctrl Pts',(-0.403519443276805,1.44937890472874,
3.70374812760043));
#98841=CARTESIAN_POINT('Ctrl Pts',(-1.43644753741059,0.447376378035769,
3.78311386834117));
#98842=CARTESIAN_POINT('Ctrl Pts',(-1.15513898747168,-0.963940386110368,
3.86247960908191));
#98843=CARTESIAN_POINT('Ctrl Pts',(0.183030980467356,-1.49332742937878,
3.94184534982265));
#98844=CARTESIAN_POINT('Ctrl Pts',(1.3537419857313,-0.656437196041839,4.0212110905634));
#98845=CARTESIAN_POINT('Ctrl Pts',(1.28588542136093,0.781041496225876,4.10057683130413));
#98846=CARTESIAN_POINT('Ctrl Pts',(0.0415447385531691,1.5039285868089,4.17994257204488));
#98847=CARTESIAN_POINT('Ctrl Pts',(-1.24080614844871,0.850839166301608,
4.25930831278561));
#98848=CARTESIAN_POINT('Ctrl Pts',(-1.38791683146307,-0.580701226943189,
4.33867405352636));
#98849=CARTESIAN_POINT('Ctrl Pts',(-0.265192772225267,-1.4809456554619,
4.41803979426709));
#98850=CARTESIAN_POINT('Ctrl Pts',(1.10016206232645,-1.02624109186263,4.49740553500784));
#98851=CARTESIAN_POINT('Ctrl Pts',(1.45895461806202,0.367393316349602,4.57677127574858));
#98852=CARTESIAN_POINT('Ctrl Pts',(0.482919130995172,1.42489194833545,4.65613701648932));
#98853=CARTESIAN_POINT('Ctrl Pts',(-0.934950964003268,1.17872592883417,
4.73550275723005));
#98854=CARTESIAN_POINT('Ctrl Pts',(-1.49741144184235,-0.145880824134014,
4.8148684979708));
#98855=CARTESIAN_POINT('Ctrl Pts',(-0.689863691058279,-1.33701976988246,
4.89423423871154));
#98856=CARTESIAN_POINT('Ctrl Pts',(0.748865796737256,-1.3048874583879,4.97359997945228));
#98857=CARTESIAN_POINT('Ctrl Pts',(1.50242161766438,-0.0788917537964559,
5.05296572019302));
#98858=CARTESIAN_POINT('Ctrl Pts',(0.881418347818994,1.21929534908143,5.13233146093376));
#98859=CARTESIAN_POINT('Ctrl Pts',(-0.546087068047113,1.40190083168179,
5.2116972016745));
#98860=CARTESIAN_POINT('Ctrl Pts',(-1.4738255476685,0.301919410773503,5.29106294241524));
#98861=CARTESIAN_POINT('Ctrl Pts',(-1.05339640289514,-1.07437494959065,
5.37042868315598));
#98862=CARTESIAN_POINT('Ctrl Pts',(0.331316329833411,-1.46754750574636,
5.44979442389673));
#98863=CARTESIAN_POINT('Ctrl Pts',(1.41192976903645,-0.518321256978449,
5.52916016463746));
#98864=CARTESIAN_POINT('Ctrl Pts',(1.20260696460544,0.905686214543761,5.60852590537821));
#98865=CARTESIAN_POINT('Ctrl Pts',(-0.110734997592681,1.49997996721392,
5.68789164611894));
#98866=CARTESIAN_POINT('Ctrl Pts',(-0.913105532322684,0.982786436071908,
5.74080213994611));
#98867=CARTESIAN_POINT('Ctrl Pts',(-1.11643975271933,0.611630017696981,
5.76725738685969));
#98868=CARTESIAN_POINT('Ctrl Pts',(0.68466442453946,-0.958295198918397,
1.5365));
#98869=CARTESIAN_POINT('Ctrl Pts',(1.0032462494074,-0.730680950158591,1.56295524691358));
#98870=CARTESIAN_POINT('Ctrl Pts',(1.39008345281789,0.0632809226906779,
1.61586574074074));
#98871=CARTESIAN_POINT('Ctrl Pts',(0.699684352884252,1.20436024859309,1.69523148148148));
#98872=CARTESIAN_POINT('Ctrl Pts',(-0.631454764128155,1.24000070664669,
1.77459722222222));
#98873=CARTESIAN_POINT('Ctrl Pts',(-1.3845553503663,0.142915811403915,1.85396296296296));
#98874=CARTESIAN_POINT('Ctrl Pts',(-0.871057879031703,-1.08584979452172,
1.9333287037037));
#98875=CARTESIAN_POINT('Ctrl Pts',(0.439473835276103,-1.32066405983435,
2.01269444444444));
#98876=CARTESIAN_POINT('Ctrl Pts',(1.34787702874157,-0.347428546246197,
2.09206018518518));
#98877=CARTESIAN_POINT('Ctrl Pts',(1.02310199861475,0.943810199691403,2.17142592592593));
#98878=CARTESIAN_POINT('Ctrl Pts',(-0.237743248735789,1.37146670874731,
2.25079166666666));
#98879=CARTESIAN_POINT('Ctrl Pts',(-1.28106565940202,0.544375715135843,
2.33015740740741));
#98880=CARTESIAN_POINT('Ctrl Pts',(-1.15231702117895,-0.780795606940967,
2.40952314814815));
#98881=CARTESIAN_POINT('Ctrl Pts',(0.0307129365700887,-1.39159014732659,
2.48888888888889));
#98882=CARTESIAN_POINT('Ctrl Pts',(1.18564203741949,-0.729194359677473,
2.56825462962963));
#98883=CARTESIAN_POINT('Ctrl Pts',(1.25580231344031,0.600359775536952,2.64762037037037));
#98884=CARTESIAN_POINT('Ctrl Pts',(0.177001877056122,1.3806304142218,2.72698611111111));
#98885=CARTESIAN_POINT('Ctrl Pts',(-1.06374123565895,0.897733463996245,
2.80635185185185));
#98886=CARTESIAN_POINT('Ctrl Pts',(-1.3312447611204,-0.40651948076358,2.88571759259259));
#98887=CARTESIAN_POINT('Ctrl Pts',(-0.380763881655566,-1.33883882596208,
2.96508333333333));
#98888=CARTESIAN_POINT('Ctrl Pts',(0.918086015388248,-1.04622594248328,
3.04444907407407));
#98889=CARTESIAN_POINT('Ctrl Pts',(1.37695934771338,0.203601540672618,3.12381481481481));
#98890=CARTESIAN_POINT('Ctrl Pts',(0.576023051783349,1.26714957918899,3.20318055555555));
#98891=CARTESIAN_POINT('Ctrl Pts',(-0.751929078651436,1.17135532206144,
3.2825462962963));
#98892=CARTESIAN_POINT('Ctrl Pts',(-1.39192517865002,0.00386296384616128,
3.36191203703703));
#98893=CARTESIAN_POINT('Ctrl Pts',(-0.758419095463071,-1.16716369832806,
3.44127777777778));
#98894=CARTESIAN_POINT('Ctrl Pts',(0.568980874699694,-1.27032727667186,
3.52064351851852));
#98895=CARTESIAN_POINT('Ctrl Pts',(1.37580804658996,-0.211241198394891,
3.60000925925926));
#98896=CARTESIAN_POINT('Ctrl Pts',(0.92387894541309,1.04111397962895,3.679375));
#98897=CARTESIAN_POINT('Ctrl Pts',(-0.373326806220943,1.34093166146447,
3.75874074074074));
#98898=CARTESIAN_POINT('Ctrl Pts',(-1.32896786110395,0.413902222491454,
3.83810648148148));
#98899=CARTESIAN_POINT('Ctrl Pts',(-1.06870773173194,-0.891815231532984,
3.91747222222222));
#98900=CARTESIAN_POINT('Ctrl Pts',(0.169336007262713,-1.38159181457256,
3.99683796296296));
#98901=CARTESIAN_POINT('Ctrl Pts',(1.25245060777301,-0.607320430195027,
4.0762037037037));
#98902=CARTESIAN_POINT('Ctrl Pts',(1.18967129222925,0.72260143140615,4.15556944444444));
#98903=CARTESIAN_POINT('Ctrl Pts',(0.0384362261044693,1.39139975892709,
4.23493518518518));
#98904=CARTESIAN_POINT('Ctrl Pts',(-1.14796499712134,0.787176612813602,
4.31430092592593));
#98905=CARTESIAN_POINT('Ctrl Pts',(-1.28406838040505,-0.537251272609856,
4.39366666666667));
#98906=CARTESIAN_POINT('Ctrl Pts',(-0.245350186557975,-1.37013648524764,
4.47303240740741));
#98907=CARTESIAN_POINT('Ctrl Pts',(1.01784435891986,-0.949454395868983,
4.55239814814815));
#98908=CARTESIAN_POINT('Ctrl Pts',(1.3497908887844,0.339903753598391,4.63176388888888));
#98909=CARTESIAN_POINT('Ctrl Pts',(0.446785551083708,1.31827689878403,4.71112962962963));
#98910=CARTESIAN_POINT('Ctrl Pts',(-0.864994892266185,1.09052982143318,
4.79049537037036));
#98911=CARTESIAN_POINT('Ctrl Pts',(-1.38537024794173,-0.134965546444495,
4.86986111111111));
#98912=CARTESIAN_POINT('Ctrl Pts',(-0.63824584614602,-1.2369796024973,4.94922685185185));
#98913=CARTESIAN_POINT('Ctrl Pts',(0.692833222393801,-1.20725153504819,
5.0285925925926));
#98914=CARTESIAN_POINT('Ctrl Pts',(1.39000554611486,-0.0729888162087741,
5.10795833333333));
#98915=CARTESIAN_POINT('Ctrl Pts',(0.815467760521459,1.12806370571929,5.18732407407407));
#98916=CARTESIAN_POINT('Ctrl Pts',(-0.505227057653176,1.2970060522492,5.26668981481481));
#98917=CARTESIAN_POINT('Ctrl Pts',(-1.36354912707508,0.279328818569119,
5.34605555555555));
#98918=CARTESIAN_POINT('Ctrl Pts',(-0.974577858216613,-0.993986721822778,
5.42542129629629));
#98919=CARTESIAN_POINT('Ctrl Pts',(0.306526164541481,-1.35774082866675,
5.50478703703704));
#98920=CARTESIAN_POINT('Ctrl Pts',(1.30628459189527,-0.479538774867528,
5.58415277777777));
#98921=CARTESIAN_POINT('Ctrl Pts',(1.11262400044309,0.837919826534893,5.66351851851852));
#98922=CARTESIAN_POINT('Ctrl Pts',(-0.102449444944844,1.38774658789174,
5.74288425925926));
#98923=CARTESIAN_POINT('Ctrl Pts',(-0.844784006828786,0.909251158746022,
5.79579475308642));
#98924=CARTESIAN_POINT('Ctrl Pts',(-1.03290409957988,0.565865870654058,
5.82225));
#98925=CARTESIAN_POINT('',(0.684664424539459,-0.958295198918398,1.5365));
#98926=CARTESIAN_POINT('Ctrl Pts',(0.68466442453946,-0.958295198918397,
1.5365));
#98927=CARTESIAN_POINT('Ctrl Pts',(1.0032462494074,-0.730680950158591,1.56295524691358));
#98928=CARTESIAN_POINT('Ctrl Pts',(1.39008345281789,0.0632809226906779,
1.61586574074074));
#98929=CARTESIAN_POINT('Ctrl Pts',(0.699684352884252,1.20436024859309,1.69523148148148));
#98930=CARTESIAN_POINT('Ctrl Pts',(-0.631454764128155,1.24000070664669,
1.77459722222222));
#98931=CARTESIAN_POINT('Ctrl Pts',(-1.15936325402709,0.47096607711394,1.83023102348301));
#98932=CARTESIAN_POINT('Ctrl Pts',(-1.17944031356009,0.040928653270331,
1.85940957783022));
#98933=CARTESIAN_POINT('Ctrl Pts',(-1.17916256915606,0.000764266613825456,
1.86213288526384));
#98934=CARTESIAN_POINT('Ctrl Pts',(0.635549693826274,1.32090956116917,1.5365));
#98935=CARTESIAN_POINT('Ctrl Pts',(0.668371665271443,1.30136299053671,1.5365));
#98936=CARTESIAN_POINT('Ctrl Pts',(0.700319009618862,1.28047972670152,1.5365));
#98937=CARTESIAN_POINT('Ctrl Pts',(0.731298112320437,1.258254780263,1.5365));
#98938=CARTESIAN_POINT('Ctrl Pts',(0.778115193593959,1.22466739286398,1.5365));
#98939=CARTESIAN_POINT('Ctrl Pts',(0.8227230333276,1.18801677550436,1.5365));
#98940=CARTESIAN_POINT('Ctrl Pts',(0.864970762882032,1.14861428602645,1.5365));
#98941=CARTESIAN_POINT('Ctrl Pts',(0.888238976066587,1.12691310741061,1.5365));
#98942=CARTESIAN_POINT('Ctrl Pts',(0.910790566548664,1.10437663719369,1.5365));
#98943=CARTESIAN_POINT('Ctrl Pts',(0.932594554500452,1.08105394609257,1.5365));
#98944=CARTESIAN_POINT('Ctrl Pts',(0.941462884755166,1.07156791410746,1.5365));
#98945=CARTESIAN_POINT('Ctrl Pts',(0.950201883404501,1.06195772650583,1.5365));
#98946=CARTESIAN_POINT('Ctrl Pts',(0.958806250728338,1.05223126289076,1.5365));
#98947=CARTESIAN_POINT('Ctrl Pts',(0.996950496046642,1.00911262322217,1.5365));
#98948=CARTESIAN_POINT('Ctrl Pts',(1.03247665648105,0.9636850768696,1.5365));
#98949=CARTESIAN_POINT('Ctrl Pts',(1.06523098522607,0.916259923496862,1.5365));
#98950=CARTESIAN_POINT('Ctrl Pts',(1.08680272763468,0.88502609177314,1.5365));
#98951=CARTESIAN_POINT('Ctrl Pts',(1.10717129187612,0.852925200570024,1.5365));
#98952=CARTESIAN_POINT('Ctrl Pts',(1.12628097828619,0.820042442228975,1.5365));
#98953=CARTESIAN_POINT('Ctrl Pts',(1.13512109289053,0.804830923525629,1.5365));
#98954=CARTESIAN_POINT('Ctrl Pts',(1.14369167315765,0.789452063683111,1.5365));
#98955=CARTESIAN_POINT('Ctrl Pts',(1.15198647178161,0.773914235960689,1.5365));
#98956=CARTESIAN_POINT('Ctrl Pts',(1.15740362680874,0.763766814019196,1.5365));
#98957=CARTESIAN_POINT('Ctrl Pts',(1.16269966037558,0.753558008249274,1.5365));
#98958=CARTESIAN_POINT('Ctrl Pts',(1.16787023655212,0.743296596712718,1.5365));
#98959=CARTESIAN_POINT('Ctrl Pts',(1.19317330635655,0.693080681979709,1.5365));
#98960=CARTESIAN_POINT('Ctrl Pts',(1.21550092753937,0.641559462581337,1.5365));
#98961=CARTESIAN_POINT('Ctrl Pts',(1.23470656272152,0.589020877926899,1.5365));
#98962=CARTESIAN_POINT('Ctrl Pts',(1.25341209489621,0.537850365921132,1.5365));
#98963=CARTESIAN_POINT('Ctrl Pts',(1.26915622673503,0.485713750528139,1.5365));
#98964=CARTESIAN_POINT('Ctrl Pts',(1.28175524628345,0.432872280614102,1.5365));
#98965=CARTESIAN_POINT('Ctrl Pts',(1.28901069367532,0.402442253611051,1.5365));
#98966=CARTESIAN_POINT('Ctrl Pts',(1.29522221805268,0.371778468368829,1.5365));
#98967=CARTESIAN_POINT('Ctrl Pts',(1.30034693367704,0.340932012339273,1.5365));
#98968=CARTESIAN_POINT('Ctrl Pts',(1.30315429133339,0.324034092366103,1.5365));
#98969=CARTESIAN_POINT('Ctrl Pts',(1.30563540254653,0.307081378175802,1.5365));
#98970=CARTESIAN_POINT('Ctrl Pts',(1.30778245093735,0.290082502724922,1.5365));
#98971=CARTESIAN_POINT('Ctrl Pts',(1.30953853292398,0.276179034549808,1.5365));
#98972=CARTESIAN_POINT('Ctrl Pts',(1.31107148447691,0.262239050551849,1.5365));
#98973=CARTESIAN_POINT('Ctrl Pts',(1.31237423627975,0.248299738344912,1.5365));
#98974=CARTESIAN_POINT('Ctrl Pts',(1.31728054844017,0.195802695669594,1.5365));
#98975=CARTESIAN_POINT('Ctrl Pts',(1.31893767644355,0.143241374071065,1.5365));
#98976=CARTESIAN_POINT('Ctrl Pts',(1.31718629034563,0.0908600606045076,
1.5365));
#98977=CARTESIAN_POINT('Ctrl Pts',(1.31685757230311,0.081028600341348,1.5365));
#98978=CARTESIAN_POINT('Ctrl Pts',(1.31640863417287,0.0712035002648672,
1.5365));
#98979=CARTESIAN_POINT('Ctrl Pts',(1.31583821714336,0.0613864111671154,
1.5365));
#98980=CARTESIAN_POINT('Ctrl Pts',(1.31263997032252,0.00634339461558057,
1.5365));
#98981=CARTESIAN_POINT('Ctrl Pts',(1.30562707296685,-0.0484498498608809,
1.5365));
#98982=CARTESIAN_POINT('Ctrl Pts',(1.29497447721792,-0.102685066480243,
1.5365));
#98983=CARTESIAN_POINT('Ctrl Pts',(1.2901198385654,-0.127401331429526,1.5365));
#98984=CARTESIAN_POINT('Ctrl Pts',(1.28450857165666,-0.15200134371386,1.5365));
#98985=CARTESIAN_POINT('Ctrl Pts',(1.27815396025382,-0.17645366274151,1.5365));
#98986=CARTESIAN_POINT('Ctrl Pts',(1.27368779636514,-0.193639302792945,
1.5365));
#98987=CARTESIAN_POINT('Ctrl Pts',(1.26885440929981,-0.210751956731087,
1.5365));
#98988=CARTESIAN_POINT('Ctrl Pts',(1.26365790001108,-0.227780164186455,
1.5365));
#98989=CARTESIAN_POINT('Ctrl Pts',(1.26065745640051,-0.237612182839758,
1.5365));
#98990=CARTESIAN_POINT('Ctrl Pts',(1.25753832486369,-0.247408091345072,
1.5365));
#98991=CARTESIAN_POINT('Ctrl Pts',(1.25430368317161,-0.257160555646816,
1.5365));
#98992=CARTESIAN_POINT('Ctrl Pts',(1.23777055696308,-0.307008031347003,
1.5365));
#98993=CARTESIAN_POINT('Ctrl Pts',(1.21820958657514,-0.355768175917083,
1.5365));
#98994=CARTESIAN_POINT('Ctrl Pts',(1.19579278545305,-0.403182449103861,
1.5365));
#98995=CARTESIAN_POINT('Ctrl Pts',(1.17348813792584,-0.450359503734913,
1.5365));
#98996=CARTESIAN_POINT('Ctrl Pts',(1.1483553706739,-0.496205014965645,1.5365));
#98997=CARTESIAN_POINT('Ctrl Pts',(1.12052480333655,-0.540431538414555,
1.5365));
#98998=CARTESIAN_POINT('Ctrl Pts',(1.10658511428344,-0.56258358358505,1.5365));
#98999=CARTESIAN_POINT('Ctrl Pts',(1.09196806725482,-0.58432886272342,1.5365));
#99000=CARTESIAN_POINT('Ctrl Pts',(1.07668725366543,-0.605627085499898,
1.5365));
#99001=CARTESIAN_POINT('Ctrl Pts',(1.06542913651814,-0.621318520098206,
1.5365));
#99002=CARTESIAN_POINT('Ctrl Pts',(1.05381069007002,-0.636767234933413,
1.5365));
#99003=CARTESIAN_POINT('Ctrl Pts',(1.04183685019325,-0.651955973544627,
1.5365));
#99004=CARTESIAN_POINT('Ctrl Pts',(1.03604983666891,-0.659296762854099,
1.5365));
#99005=CARTESIAN_POINT('Ctrl Pts',(1.03018036182183,-0.666575950104624,
1.5365));
#99006=CARTESIAN_POINT('Ctrl Pts',(1.02423735593939,-0.673781861503873,
1.5365));
#99007=CARTESIAN_POINT('Ctrl Pts',(0.992151017998599,-0.712686636781099,
1.5365));
#99008=CARTESIAN_POINT('Ctrl Pts',(0.957862153431288,-0.749537867796629,
1.5365));
#99009=CARTESIAN_POINT('Ctrl Pts',(0.921500569781594,-0.784083458027627,
1.5365));
#99010=CARTESIAN_POINT('Ctrl Pts',(0.885879292605549,-0.81792571464339,
1.5365));
#99011=CARTESIAN_POINT('Ctrl Pts',(0.848268090926396,-0.849555837281558,
1.5365));
#99012=CARTESIAN_POINT('Ctrl Pts',(0.808765267737003,-0.878693245937888,
1.5365));
#99013=CARTESIAN_POINT('Ctrl Pts',(0.769262444547611,-0.907830654594219,
1.5365));
#99014=CARTESIAN_POINT('Ctrl Pts',(0.727867374730229,-0.934476030499942,
1.5365));
#99015=CARTESIAN_POINT('Ctrl Pts',(0.684664424539467,-0.958295198918392,
1.5365));
#99016=CARTESIAN_POINT('Ctrl Pts',(0.632684721053874,1.31669749784946,5.5365));
#99017=CARTESIAN_POINT('Ctrl Pts',(0.843561153930663,1.21579764861352,5.52384689303253));
#99018=CARTESIAN_POINT('Ctrl Pts',(1.03149297598832,1.06720222196338,5.51119378606506));
#99019=CARTESIAN_POINT('Ctrl Pts',(1.1710342653585,0.882239411150659,5.49854067909758));
#99020=CARTESIAN_POINT('Ctrl Pts',(1.46278863639303,0.495517253307565,5.472085432184));
#99021=CARTESIAN_POINT('Ctrl Pts',(1.54300437985592,-0.050184483946369,
5.44563018527042));
#99022=CARTESIAN_POINT('Ctrl Pts',(1.37605834110377,-0.504914459024216,
5.41917493835684));
#99023=CARTESIAN_POINT('Ctrl Pts',(1.20911230235162,-0.959644434102056,
5.39271969144326));
#99024=CARTESIAN_POINT('Ctrl Pts',(0.795004481384448,-1.32340264700381,
5.36626444452968));
#99025=CARTESIAN_POINT('Ctrl Pts',(0.322628878789288,-1.42994684432483,
5.3398091976161));
#99026=CARTESIAN_POINT('Ctrl Pts',(-0.149746723805883,-1.53649104164586,
5.31335395070252));
#99027=CARTESIAN_POINT('Ctrl Pts',(-0.680390108029043,-1.38582122338613,
5.28689870378894));
#99028=CARTESIAN_POINT('Ctrl Pts',(-1.02626928290781,-1.04677764753815,
5.26044345687536));
#99029=CARTESIAN_POINT('Ctrl Pts',(-1.30208279114181,-0.776415032814075,
5.23934731986454));
#99030=CARTESIAN_POINT('Ctrl Pts',(-1.46040652113662,-0.386267362945073,
5.21825118285372));
#99031=CARTESIAN_POINT('Ctrl Pts',(-1.46394239258928,0.00129898642790893,
5.19715504584291));
#99032=CARTESIAN_POINT('Origin',(0.,0.,0.612132885263843));
#99033=CARTESIAN_POINT('',(-0.684664424539452,-0.958295198918403,1.5365));
#99034=CARTESIAN_POINT('Ctrl Pts',(-0.686152415706125,-0.959598509482521,
1.5365));
#99035=CARTESIAN_POINT('Ctrl Pts',(-0.391329521689054,-1.16791585444763,
1.56098466970649));
#99036=CARTESIAN_POINT('Ctrl Pts',(0.438700349941051,-1.30460055950163,
1.61196176702858));
#99037=CARTESIAN_POINT('Ctrl Pts',(1.34228035673205,-0.370854820156928,
1.68943129196628));
#99038=CARTESIAN_POINT('Ctrl Pts',(1.03835463241157,0.928154933276721,1.76890857481307));
#99039=CARTESIAN_POINT('Ctrl Pts',(-0.218198112454921,1.37532415660838,
1.84838585765988));
#99040=CARTESIAN_POINT('Ctrl Pts',(-1.06862547075175,0.719869665458091,
1.91237203763424));
#99041=CARTESIAN_POINT('Ctrl Pts',(-1.17668973402415,0.163910804078405,
1.949865789993));
#99042=CARTESIAN_POINT('Ctrl Pts',(-1.17603208311293,0.000536542008743694,
1.96086711473616));
#99043=CARTESIAN_POINT('Origin',(0.,0.,1.5365));
#99044=CARTESIAN_POINT('Origin',(-0.577350269189626,-1.,0.));
#99045=CARTESIAN_POINT('',(-0.577350269189626,-1.,0.));
#99046=CARTESIAN_POINT('',(0.577350269189626,-1.,0.));
#99047=CARTESIAN_POINT('',(1.21132486540519,-1.,0.));
#99048=CARTESIAN_POINT('',(-0.577350269189626,-1.,1.));
#99049=CARTESIAN_POINT('',(-0.577350269189626,-1.,0.));
#99050=CARTESIAN_POINT('',(0.577350269189626,-1.,1.));
#99051=CARTESIAN_POINT('',(-0.577350269189626,-1.,1.));
#99052=CARTESIAN_POINT('',(0.577350269189626,-1.,0.));
#99053=CARTESIAN_POINT('Origin',(-1.15470053837925,1.41410031829988E-16,
0.));
#99054=CARTESIAN_POINT('',(-1.15470053837925,1.41410031829988E-16,0.));
#99055=CARTESIAN_POINT('',(-0.635362971081846,-0.899519052838328,0.));
#99056=CARTESIAN_POINT('',(-1.15470053837925,1.38777878078145E-16,1.));
#99057=CARTESIAN_POINT('',(-1.15470053837925,1.41410031829988E-16,0.));
#99058=CARTESIAN_POINT('',(-1.15470053837925,1.41410031829988E-16,1.));
#99059=CARTESIAN_POINT('Origin',(-0.577350269189626,1.,0.));
#99060=CARTESIAN_POINT('',(-0.577350269189626,1.,0.));
#99061=CARTESIAN_POINT('',(-0.346687836487032,1.39951905283833,0.));
#99062=CARTESIAN_POINT('',(-0.577350269189626,1.,1.));
#99063=CARTESIAN_POINT('',(-0.577350269189626,1.,0.));
#99064=CARTESIAN_POINT('',(-0.577350269189626,1.,1.));
#99065=CARTESIAN_POINT('Origin',(0.577350269189626,1.,0.));
#99066=CARTESIAN_POINT('',(0.577350269189626,1.,0.));
#99067=CARTESIAN_POINT('',(1.78867513459481,1.,0.));
#99068=CARTESIAN_POINT('',(0.577350269189626,1.,1.));
#99069=CARTESIAN_POINT('',(0.577350269189626,1.,0.));
#99070=CARTESIAN_POINT('',(0.577350269189626,1.,1.));
#99071=CARTESIAN_POINT('Origin',(1.15470053837925,0.,0.));
#99072=CARTESIAN_POINT('',(1.15470053837925,0.,0.));
#99073=CARTESIAN_POINT('',(1.38536297108184,-0.399519052838329,0.));
#99074=CARTESIAN_POINT('',(1.15470053837925,0.,1.));
#99075=CARTESIAN_POINT('',(1.15470053837925,0.,0.));
#99076=CARTESIAN_POINT('',(1.15470053837925,0.,1.));
#99077=CARTESIAN_POINT('Origin',(0.577350269189626,-1.,0.));
#99078=CARTESIAN_POINT('',(1.09668783648703,-0.100480947161671,0.));
#99079=CARTESIAN_POINT('',(0.577350269189626,-1.,1.));
#99080=CARTESIAN_POINT('Origin',(0.,0.,1.));
#99081=CARTESIAN_POINT('Ctrl Pts',(-0.510216505388432,1.06149619882938,
1.37152216057906));
#99082=CARTESIAN_POINT('Ctrl Pts',(-0.863603094147857,0.891638152642483,
1.39801458819466));
#99083=CARTESIAN_POINT('Ctrl Pts',(-1.3812395390238,0.174157193963341,1.45099944342587));
#99084=CARTESIAN_POINT('Ctrl Pts',(-0.893256777570882,-1.06957578104115,
1.53047672627267));
#99085=CARTESIAN_POINT('Ctrl Pts',(0.415282497480903,-1.32880020955467,
1.60995400911947));
#99086=CARTESIAN_POINT('Ctrl Pts',(1.34228035673205,-0.370854820156928,
1.68943129196628));
#99087=CARTESIAN_POINT('Ctrl Pts',(1.03835463241157,0.928154933276721,1.76890857481307));
#99088=CARTESIAN_POINT('Ctrl Pts',(-0.218198112454921,1.37532415660838,
1.84838585765988));
#99089=CARTESIAN_POINT('Ctrl Pts',(-1.27451458146588,0.561183634276331,
1.92786314050668));
#99090=CARTESIAN_POINT('Ctrl Pts',(-1.16179386595564,-0.767846081811985,
2.00734042335348));
#99091=CARTESIAN_POINT('Ctrl Pts',(0.0166383981799684,-1.39248065884836,
2.08681770620029));
#99092=CARTESIAN_POINT('Ctrl Pts',(1.17979588449659,-0.739859513451799,
2.16629498904709));
#99093=CARTESIAN_POINT('Ctrl Pts',(1.2607599562499,0.591436597715745,2.24577227189389));
#99094=CARTESIAN_POINT('Ctrl Pts',(0.185253888314333,1.38021153969935,2.32524955474069));
#99095=CARTESIAN_POINT('Ctrl Pts',(-1.06017953986855,0.902954733563308,
2.4047268375875));
#99096=CARTESIAN_POINT('Ctrl Pts',(-1.33313519782792,-0.402564735116712,
2.4842041204343));
#99097=CARTESIAN_POINT('Ctrl Pts',(-0.383235548912603,-1.33881925708758,
2.5636814032811));
#99098=CARTESIAN_POINT('Ctrl Pts',(0.918197143413365,-1.04700586255646,
2.6431586861279));
#99099=CARTESIAN_POINT('Ctrl Pts',(1.37738848098126,0.205202743845419,2.7226359689747));
#99100=CARTESIAN_POINT('Ctrl Pts',(0.573132410162518,1.26918330522814,2.80211325182151));
#99101=CARTESIAN_POINT('Ctrl Pts',(-0.756845033196452,1.16897080220297,
2.88159053466831));
#99102=CARTESIAN_POINT('Ctrl Pts',(-1.39258564709099,-0.0035122637810132,
2.96106781751511));
#99103=CARTESIAN_POINT('Ctrl Pts',(-0.750938898498722,-1.17277357998896,
3.04054510036192));
#99104=CARTESIAN_POINT('Ctrl Pts',(0.579527130353369,-1.26627620290932,
3.12002238320872));
#99105=CARTESIAN_POINT('Ctrl Pts',(1.37840601855021,-0.198252265336022,
3.19949966605552));
#99106=CARTESIAN_POINT('Ctrl Pts',(0.912904206293459,1.0516239918919,3.27897694890232));
#99107=CARTESIAN_POINT('Ctrl Pts',(-0.389984008629303,1.33686932263319,
3.35845423174912));
#99108=CARTESIAN_POINT('Ctrl Pts',(-1.33514870363572,0.395834625998962,
3.43793151459593));
#99109=CARTESIAN_POINT('Ctrl Pts',(-1.05561165720655,-0.908290229433893,
3.51740879744272));
#99110=CARTESIAN_POINT('Ctrl Pts',(0.192214113207023,-1.37926097853155,
3.59688608028953));
#99111=CARTESIAN_POINT('Ctrl Pts',(1.26372622016576,-0.585066792922831,
3.67636336313633));
#99112=CARTESIAN_POINT('Ctrl Pts',(1.17605081651368,0.745795943229381,3.75584064598314));
#99113=CARTESIAN_POINT('Ctrl Pts',(0.00961056866032201,1.39255691077756,
3.83531792882993));
#99114=CARTESIAN_POINT('Ctrl Pts',(-1.1656452359731,0.761956884635964,3.91479521167675));
#99115=CARTESIAN_POINT('Ctrl Pts',(-1.2716810021026,-0.567568975171852,
3.99427249452353));
#99116=CARTESIAN_POINT('Ctrl Pts',(-0.211232513047386,-1.37647664066694,
4.07374977737036));
#99117=CARTESIAN_POINT('Ctrl Pts',(1.042974782858,-0.922773374952316,4.15322706021714));
#99118=CARTESIAN_POINT('Ctrl Pts',(1.34048488368858,0.37736904627051,4.23270434306396));
#99119=CARTESIAN_POINT('Ctrl Pts',(0.40839846752904,1.33135939264991,4.31218162591074));
#99120=CARTESIAN_POINT('Ctrl Pts',(-0.898302601136657,1.0641237985496,4.39165890875756));
#99121=CARTESIAN_POINT('Ctrl Pts',(-1.38101105538947,-0.179208421994024,
4.47113619160435));
#99122=CARTESIAN_POINT('Ctrl Pts',(-0.596949142579923,-1.25815698208656,
4.55061347445117));
#99123=CARTESIAN_POINT('Ctrl Pts',(0.734680490718179,-1.18302623202404,
4.63009075729796));
#99124=CARTESIAN_POINT('Ctrl Pts',(1.39240476784912,-0.0227328862735182,
4.70956804014477));
#99125=CARTESIAN_POINT('Ctrl Pts',(0.772906734413495,1.15841403976235,4.78904532299156));
#99126=CARTESIAN_POINT('Ctrl Pts',(-0.555559517726036,1.27697162056126,
4.86852260583837));
#99127=CARTESIAN_POINT('Ctrl Pts',(-1.37442674999021,0.224196398972394,
4.94799988868517));
#99128=CARTESIAN_POINT('Ctrl Pts',(-0.932557331581966,-1.03423752205814,
5.02747717153198));
#99129=CARTESIAN_POINT('Ctrl Pts',(0.364714346074539,-1.34397271822316,
5.10695445437878));
#99130=CARTESIAN_POINT('Ctrl Pts',(1.32746371769155,-0.420942597676582,
5.18643173722558));
#99131=CARTESIAN_POINT('Ctrl Pts',(1.07251885993521,0.888266730679483,5.26590902007238));
#99132=CARTESIAN_POINT('Ctrl Pts',(-0.166143802083737,1.38257845674616,
5.34538630291918));
#99133=CARTESIAN_POINT('Ctrl Pts',(-1.25255794971928,0.608892852159982,
5.42486358576599));
#99134=CARTESIAN_POINT('Ctrl Pts',(-1.18974047573171,-0.723717800049171,
5.50434086861279));
#99135=CARTESIAN_POINT('Ctrl Pts',(-0.0361513007060795,-1.39171212292046,
5.58381815145959));
#99136=CARTESIAN_POINT('Ctrl Pts',(1.15165463117661,-0.784596477531957,
5.66329543430639));
#99137=CARTESIAN_POINT('Ctrl Pts',(1.28099440281734,0.545166701406554,5.7427727171532));
#99138=CARTESIAN_POINT('Ctrl Pts',(0.586914422573267,1.09378259267779,5.7957575723844));
#99139=CARTESIAN_POINT('Ctrl Pts',(0.200551794415766,1.1605490253568,5.82225));
#99140=CARTESIAN_POINT('Ctrl Pts',(-0.551480035117359,1.14734422509853,
1.42651477371938));
#99141=CARTESIAN_POINT('Ctrl Pts',(-0.933446604839922,0.963748986044478,
1.45300720133498));
#99142=CARTESIAN_POINT('Ctrl Pts',(-1.49294666370392,0.188242078467704,
1.50599205656618));
#99143=CARTESIAN_POINT('Ctrl Pts',(-0.965498516533845,-1.1560772398772,
1.58546933941298));
#99144=CARTESIAN_POINT('Ctrl Pts',(0.448868282142376,-1.43626632711789,
1.66494662225978));
#99145=CARTESIAN_POINT('Ctrl Pts',(1.45083667511772,-0.400847536454914,
1.74442390510659));
#99146=CARTESIAN_POINT('Ctrl Pts',(1.1223310949352,1.00321904484081,1.82390118795339));
#99147=CARTESIAN_POINT('Ctrl Pts',(-0.235844786376658,1.48655287740392,
1.90337847080019));
#99148=CARTESIAN_POINT('Ctrl Pts',(-1.37759037334414,0.606569107564232,
1.98285575364699));
#99149=CARTESIAN_POINT('Ctrl Pts',(-1.25575342081217,-0.829945287324689,
2.06233303649379));
#99150=CARTESIAN_POINT('Ctrl Pts',(0.0179840211276536,-1.50509690402374,
2.1418103193406));
#99151=CARTESIAN_POINT('Ctrl Pts',(1.27521134448241,-0.799695317872338,
2.2212876021874));
#99152=CARTESIAN_POINT('Ctrl Pts',(1.36272334901815,0.639268765775537,2.3007648850342));
#99153=CARTESIAN_POINT('Ctrl Pts',(0.200236212968925,1.49183552539781,2.38024216788101));
#99154=CARTESIAN_POINT('Ctrl Pts',(-1.14592108193815,0.975980790342683,
2.45971945072781));
#99155=CARTESIAN_POINT('Ctrl Pts',(-1.44095190561235,-0.435121976483607,
2.53919673357461));
#99156=CARTESIAN_POINT('Ctrl Pts',(-0.414229551064106,-1.44709566060072,
2.61867401642141));
#99157=CARTESIAN_POINT('Ctrl Pts',(0.992455923213934,-1.13168198941574,
2.69815129926821));
#99158=CARTESIAN_POINT('Ctrl Pts',(1.48878415307929,0.221798423192708,2.77762858211502));
#99159=CARTESIAN_POINT('Ctrl Pts',(0.619484235310456,1.37182793254546,2.85710586496182));
#99160=CARTESIAN_POINT('Ctrl Pts',(-0.818054533864638,1.26351078854119,
2.93658314780862));
#99161=CARTESIAN_POINT('Ctrl Pts',(-1.50521038314314,-0.00379631653001373,
3.01606043065543));
#99162=CARTESIAN_POINT('Ctrl Pts',(-0.811670743187329,-1.26762111426529,
3.09553771350223));
#99163=CARTESIAN_POINT('Ctrl Pts',(0.626396125612256,-1.36868571963793,
3.17501499634903));
#99164=CARTESIAN_POINT('Ctrl Pts',(1.48988398354015,-0.214285827869038,
3.25449227919583));
#99165=CARTESIAN_POINT('Ctrl Pts',(0.986734922191957,1.13667360787806,3.33396956204264));
#99166=CARTESIAN_POINT('Ctrl Pts',(-0.421523789416343,1.44498802607688,
3.41344684488943));
#99167=CARTESIAN_POINT('Ctrl Pts',(-1.44312825279412,0.427847572826733,
3.49292412773624));
#99168=CARTESIAN_POINT('Ctrl Pts',(-1.14098377382632,-0.981747792035103,
3.57240141058304));
#99169=CARTESIAN_POINT('Ctrl Pts',(0.207759342910239,-1.49080808802434,
3.65187869342985));
#99170=CARTESIAN_POINT('Ctrl Pts',(1.3659295081902,-0.632383805893245,3.73135597627665));
#99171=CARTESIAN_POINT('Ctrl Pts',(1.27116339581568,0.806111853730416,3.81083325912345));
#99172=CARTESIAN_POINT('Ctrl Pts',(0.0103878190656723,1.50517932279332,
3.89031054197025));
#99173=CARTESIAN_POINT('Ctrl Pts',(-1.25991626864255,0.823579803983517,
3.96978782481705));
#99174=CARTESIAN_POINT('Ctrl Pts',(-1.37452762952801,-0.613470860024422,
4.04926510766386));
#99175=CARTESIAN_POINT('Ctrl Pts',(-0.228315847259036,-1.48779856809086,
4.12874239051066));
#99176=CARTESIAN_POINT('Ctrl Pts',(1.12732489796496,-0.997402255414395,
4.20821967335746));
#99177=CARTESIAN_POINT('Ctrl Pts',(1.44889599400175,0.407888597667038,4.28769695620426));
#99178=CARTESIAN_POINT('Ctrl Pts',(0.44142750937336,1.43903248299158,4.36717423905106));
#99179=CARTESIAN_POINT('Ctrl Pts',(-0.970952418804468,1.1501843307609,4.44665152189787));
#99180=CARTESIAN_POINT('Ctrl Pts',(-1.49269970155873,-0.193701822286891,
4.52612880474467));
#99181=CARTESIAN_POINT('Ctrl Pts',(-0.645227135219061,-1.35990986049348,
4.60560608759147));
#99182=CARTESIAN_POINT('Ctrl Pts',(0.794097444011241,-1.27870294490902,
4.68508337043828));
#99183=CARTESIAN_POINT('Ctrl Pts',(1.50501487537417,-0.0245713981967256,
4.76456065328508));
#99184=CARTESIAN_POINT('Ctrl Pts',(0.835415217922637,1.25210025270004,4.84403793613188));
#99185=CARTESIAN_POINT('Ctrl Pts',(-0.600490143124806,1.38024612436806,
4.92351521897869));
#99186=CARTESIAN_POINT('Ctrl Pts',(-1.48558289343029,0.242328181610582,
5.00299250182548));
#99187=CARTESIAN_POINT('Ctrl Pts',(-1.0079774851232,-1.11788101513904,5.08246978467229));
#99188=CARTESIAN_POINT('Ctrl Pts',(0.394210454300898,-1.45266590558106,
5.16194706751908));
#99189=CARTESIAN_POINT('Ctrl Pts',(1.43482174707819,-0.454986140388277,
5.2414243503659));
#99190=CARTESIAN_POINT('Ctrl Pts',(1.15925833894929,0.960104901850968,5.32090163321269));
#99191=CARTESIAN_POINT('Ctrl Pts',(-0.179580607134444,1.49439386579314,
5.4003789160595));
#99192=CARTESIAN_POINT('Ctrl Pts',(-1.35385800890905,0.658136786923932,
5.4798561989063));
#99193=CARTESIAN_POINT('Ctrl Pts',(-1.28596020004795,-0.782248150679337,
5.5593334817531));
#99194=CARTESIAN_POINT('Ctrl Pts',(-0.0390750208438495,-1.50426621309934,
5.63881076459991));
#99195=CARTESIAN_POINT('Ctrl Pts',(1.24479417999391,-0.848050363742887,
5.71828804744671));
#99196=CARTESIAN_POINT('Ctrl Pts',(1.38459424732454,0.589256812473393,5.79776533029351));
#99197=CARTESIAN_POINT('Ctrl Pts',(0.634380861758244,1.18224176648594,5.85075018552471));
#99198=CARTESIAN_POINT('Ctrl Pts',(0.216771330325854,1.25440790429141,5.87724261314031));
#99199=CARTESIAN_POINT('Ctrl Pts',(-0.592743564846286,1.23319225136769,
1.48150738685969));
#99200=CARTESIAN_POINT('Ctrl Pts',(-1.00329011553199,1.03585981944647,1.50799981447529));
#99201=CARTESIAN_POINT('Ctrl Pts',(-1.60465378838404,0.202326962972067,
1.56098466970649));
#99202=CARTESIAN_POINT('Ctrl Pts',(-1.03774025549681,-1.24257869871326,
1.64046195255329));
#99203=CARTESIAN_POINT('Ctrl Pts',(0.482454066803851,-1.54373244468111,
1.71993923540009));
#99204=CARTESIAN_POINT('Ctrl Pts',(1.55939299350339,-0.430840252752899,
1.7994165182469));
#99205=CARTESIAN_POINT('Ctrl Pts',(1.20630755745883,1.0782831564049,1.8788938010937));
#99206=CARTESIAN_POINT('Ctrl Pts',(-0.253491460298395,1.59778159819946,
1.9583710839405));
#99207=CARTESIAN_POINT('Ctrl Pts',(-1.4806661652224,0.651954580852132,2.0378483667873));
#99208=CARTESIAN_POINT('Ctrl Pts',(-1.3497129756687,-0.892044492837393,
2.11732564963411));
#99209=CARTESIAN_POINT('Ctrl Pts',(0.0193296440753391,-1.61771314919912,
2.19680293248091));
#99210=CARTESIAN_POINT('Ctrl Pts',(1.37062680446823,-0.859531122292875,
2.27628021532771));
#99211=CARTESIAN_POINT('Ctrl Pts',(1.4646867417864,0.687100933835329,2.35575749817451));
#99212=CARTESIAN_POINT('Ctrl Pts',(0.215218537623519,1.60345951109627,2.43523478102132));
#99213=CARTESIAN_POINT('Ctrl Pts',(-1.23166262400776,1.04900684712206,2.51471206386812));
#99214=CARTESIAN_POINT('Ctrl Pts',(-1.54876861339678,-0.467679217850505,
2.59418934671492));
#99215=CARTESIAN_POINT('Ctrl Pts',(-0.445223553215608,-1.55537206411385,
2.67366662956172));
#99216=CARTESIAN_POINT('Ctrl Pts',(1.0667147030145,-1.21635811627501,2.75314391240853));
#99217=CARTESIAN_POINT('Ctrl Pts',(1.60017982517733,0.238394102539999,2.83262119525533));
#99218=CARTESIAN_POINT('Ctrl Pts',(0.665836060458395,1.47447255986279,2.91209847810213));
#99219=CARTESIAN_POINT('Ctrl Pts',(-0.879264034532826,1.35805077487941,
2.99157576094893));
#99220=CARTESIAN_POINT('Ctrl Pts',(-1.61783511919529,-0.00408036927901526,
3.07105304379574));
#99221=CARTESIAN_POINT('Ctrl Pts',(-0.872402587875936,-1.36246864854162,
3.15053032664254));
#99222=CARTESIAN_POINT('Ctrl Pts',(0.673265120871141,-1.47109523636653,
3.23000760948934));
#99223=CARTESIAN_POINT('Ctrl Pts',(1.6013619485301,-0.230319390402056,3.30948489233614));
#99224=CARTESIAN_POINT('Ctrl Pts',(1.06056563809045,1.22172322386422,3.38896217518295));
#99225=CARTESIAN_POINT('Ctrl Pts',(-0.453063570203383,1.55310672952058,
3.46843945802974));
#99226=CARTESIAN_POINT('Ctrl Pts',(-1.55110780195252,0.459860519654501,
3.54791674087656));
#99227=CARTESIAN_POINT('Ctrl Pts',(-1.22635589044608,-1.05520535463631,
3.62739402372335));
#99228=CARTESIAN_POINT('Ctrl Pts',(0.223304572613456,-1.60235519751713,
3.70687130657016));
#99229=CARTESIAN_POINT('Ctrl Pts',(1.46813279621464,-0.679700818863657,
3.78634858941695));
#99230=CARTESIAN_POINT('Ctrl Pts',(1.36627597511768,0.86642776423145,3.86582587226377));
#99231=CARTESIAN_POINT('Ctrl Pts',(0.0111650694710232,1.61780173480908,
3.94530315511056));
#99232=CARTESIAN_POINT('Ctrl Pts',(-1.35418730131199,0.885202723331068,
4.02478043795737));
#99233=CARTESIAN_POINT('Ctrl Pts',(-1.47737425695342,-0.659372744876989,
4.10425772080417));
#99234=CARTESIAN_POINT('Ctrl Pts',(-0.245399181470685,-1.59912049551479,
4.18373500365097));
#99235=CARTESIAN_POINT('Ctrl Pts',(1.21167501307193,-1.07203113587647,4.26321228649777));
#99236=CARTESIAN_POINT('Ctrl Pts',(1.55730710431493,0.438408149063566,4.34268956934457));
#99237=CARTESIAN_POINT('Ctrl Pts',(0.474456551217679,1.54670557333325,4.42216685219138));
#99238=CARTESIAN_POINT('Ctrl Pts',(-1.04360223647228,1.23624486297219,4.50164413503818));
#99239=CARTESIAN_POINT('Ctrl Pts',(-1.604388347728,-0.20819522257976,4.58112141788498));
#99240=CARTESIAN_POINT('Ctrl Pts',(-0.693505127858197,-1.46166273890039,
4.66059870073178));
#99241=CARTESIAN_POINT('Ctrl Pts',(0.853514397304301,-1.37437965779401,
4.74007598357859));
#99242=CARTESIAN_POINT('Ctrl Pts',(1.61762498289922,-0.0264099101199331,
4.81955326642539));
#99243=CARTESIAN_POINT('Ctrl Pts',(0.897923701431777,1.34578646563773,4.89903054927219));
#99244=CARTESIAN_POINT('Ctrl Pts',(-0.645420768523576,1.48352062817486,
4.97850783211899));
#99245=CARTESIAN_POINT('Ctrl Pts',(-1.59673903687038,0.260459964248768,
5.05798511496579));
#99246=CARTESIAN_POINT('Ctrl Pts',(-1.08339763866443,-1.20152450821994,
5.1374623978126));
#99247=CARTESIAN_POINT('Ctrl Pts',(0.423706562527259,-1.56135909293895,
5.2169396806594));
#99248=CARTESIAN_POINT('Ctrl Pts',(1.54217977646484,-0.489029683099972,
5.29641696350621));
#99249=CARTESIAN_POINT('Ctrl Pts',(1.24599781796337,1.03194307302245,5.375894246353));
#99250=CARTESIAN_POINT('Ctrl Pts',(-0.19301741218515,1.60620927484011,5.45537152919982));
#99251=CARTESIAN_POINT('Ctrl Pts',(-1.45515806809883,0.707380721687883,
5.53484881204659));
#99252=CARTESIAN_POINT('Ctrl Pts',(-1.38217992436419,-0.840778501309504,
5.61432609489343));
#99253=CARTESIAN_POINT('Ctrl Pts',(-0.0419987409816216,-1.61682030327821,
5.6938033777402));
#99254=CARTESIAN_POINT('Ctrl Pts',(1.3379337288112,-0.911504249953818,5.77328066058703));
#99255=CARTESIAN_POINT('Ctrl Pts',(1.48819409183174,0.633346923540232,5.85275794343381));
#99256=CARTESIAN_POINT('Ctrl Pts',(0.681847300943222,1.2707009402941,5.90574279866502));
#99257=CARTESIAN_POINT('Ctrl Pts',(0.232990866235942,1.34826678322601,5.93223522628062));
#99258=CARTESIAN_POINT('Ctrl Pts',(-0.634007094575213,1.31904027763685,
1.5365));
#99259=CARTESIAN_POINT('Ctrl Pts',(-1.07313362622405,1.10797065284847,1.5629924276156));
#99260=CARTESIAN_POINT('Ctrl Pts',(-1.71636091306417,0.21641184747643,1.6159772828468));
#99261=CARTESIAN_POINT('Ctrl Pts',(-1.10998199445977,-1.32908015754932,
1.6954545656936));
#99262=CARTESIAN_POINT('Ctrl Pts',(0.516039851465324,-1.65119856224433,
1.77493184854041));
#99263=CARTESIAN_POINT('Ctrl Pts',(1.66794931188906,-0.460832969050885,
1.85440913138721));
#99264=CARTESIAN_POINT('Ctrl Pts',(1.29028401998246,1.15334726796898,1.93388641423401));
#99265=CARTESIAN_POINT('Ctrl Pts',(-0.271138134220133,1.709010318995,2.01336369708081));
#99266=CARTESIAN_POINT('Ctrl Pts',(-1.58374195710066,0.697340054140035,
2.09284097992762));
#99267=CARTESIAN_POINT('Ctrl Pts',(-1.44367253052523,-0.954143698350099,
2.17231826277442));
#99268=CARTESIAN_POINT('Ctrl Pts',(0.020675267023026,-1.7303293943745,2.25179554562122));
#99269=CARTESIAN_POINT('Ctrl Pts',(1.46604226445405,-0.919366926713415,
2.33127282846802));
#99270=CARTESIAN_POINT('Ctrl Pts',(1.56665013455465,0.734933101895122,2.41075011131483));
#99271=CARTESIAN_POINT('Ctrl Pts',(0.230200862278109,1.71508349679473,2.49022739416163));
#99272=CARTESIAN_POINT('Ctrl Pts',(-1.31740416607736,1.12203290390143,2.56970467700843));
#99273=CARTESIAN_POINT('Ctrl Pts',(-1.65658532118121,-0.5002364592174,2.64918195985523));
#99274=CARTESIAN_POINT('Ctrl Pts',(-0.476217555367108,-1.66364846762698,
2.72865924270203));
#99275=CARTESIAN_POINT('Ctrl Pts',(1.14097348281507,-1.30103424313428,2.80813652554884));
#99276=CARTESIAN_POINT('Ctrl Pts',(1.71157549727537,0.254989781887289,2.88761380839565));
#99277=CARTESIAN_POINT('Ctrl Pts',(0.712187885606333,1.57711718718011,2.96709109124244));
#99278=CARTESIAN_POINT('Ctrl Pts',(-0.940473535201012,1.45259076121762,
3.04656837408925));
#99279=CARTESIAN_POINT('Ctrl Pts',(-1.73045985524743,-0.00436442202801662,
3.12604565693604));
#99280=CARTESIAN_POINT('Ctrl Pts',(-0.933134432564544,-1.45731618281794,
3.20552293978285));
#99281=CARTESIAN_POINT('Ctrl Pts',(0.720134116130028,-1.57350475309514,
3.28500022262965));
#99282=CARTESIAN_POINT('Ctrl Pts',(1.71283991352004,-0.246352952935073,
3.36447750547645));
#99283=CARTESIAN_POINT('Ctrl Pts',(1.13439635398895,1.30677283985038,3.44395478832326));
#99284=CARTESIAN_POINT('Ctrl Pts',(-0.484603350990424,1.66122543296428,
3.52343207117006));
#99285=CARTESIAN_POINT('Ctrl Pts',(-1.65908735111091,0.491873466482272,
3.60290935401687));
#99286=CARTESIAN_POINT('Ctrl Pts',(-1.31172800706584,-1.12866291723752,
3.68238663686366));
#99287=CARTESIAN_POINT('Ctrl Pts',(0.238849802316674,-1.71390230700991,
3.76186391971048));
#99288=CARTESIAN_POINT('Ctrl Pts',(1.57033608423908,-0.727017831834071,
3.84134120255726));
#99289=CARTESIAN_POINT('Ctrl Pts',(1.46138855441968,0.926743674732486,3.92081848540408));
#99290=CARTESIAN_POINT('Ctrl Pts',(0.0119423198763706,1.73042414682484,
4.00029576825087));
#99291=CARTESIAN_POINT('Ctrl Pts',(-1.44845833398143,0.946825642678623,
4.07977305109768));
#99292=CARTESIAN_POINT('Ctrl Pts',(-1.58022088437883,-0.705274629729561,
4.15925033394448));
#99293=CARTESIAN_POINT('Ctrl Pts',(-0.262482515682332,-1.71044242293871,
4.23872761679128));
#99294=CARTESIAN_POINT('Ctrl Pts',(1.29602512817888,-1.14666001633855,4.31820489963808));
#99295=CARTESIAN_POINT('Ctrl Pts',(1.6657182146281,0.468927700460095,4.39768218248489));
#99296=CARTESIAN_POINT('Ctrl Pts',(0.507485593061997,1.65437866367492,4.47715946533169));
#99297=CARTESIAN_POINT('Ctrl Pts',(-1.11625205414009,1.32230539518349,4.5566367481785));
#99298=CARTESIAN_POINT('Ctrl Pts',(-1.71607699389726,-0.222688622872627,
4.63611403102529));
#99299=CARTESIAN_POINT('Ctrl Pts',(-0.741783120497333,-1.5634156173073,
4.7155913138721));
#99300=CARTESIAN_POINT('Ctrl Pts',(0.912931350597362,-1.470056370679,4.7950685967189));
#99301=CARTESIAN_POINT('Ctrl Pts',(1.73023509042427,-0.0282484220431421,
4.8745458795657));
#99302=CARTESIAN_POINT('Ctrl Pts',(0.960432184940917,1.43947267857542,4.9540231624125));
#99303=CARTESIAN_POINT('Ctrl Pts',(-0.690351393922344,1.58679513198166,
5.0335004452593));
#99304=CARTESIAN_POINT('Ctrl Pts',(-1.70789518031047,0.278591746886957,
5.11297772810611));
#99305=CARTESIAN_POINT('Ctrl Pts',(-1.15881779220566,-1.28516800130084,
5.1924550109529));
#99306=CARTESIAN_POINT('Ctrl Pts',(0.453202670753618,-1.67005228029684,
5.27193229379972));
#99307=CARTESIAN_POINT('Ctrl Pts',(1.64953780585148,-0.523073225811667,
5.35140957664651));
#99308=CARTESIAN_POINT('Ctrl Pts',(1.33273729697745,1.10378124419394,5.43088685949333));
#99309=CARTESIAN_POINT('Ctrl Pts',(-0.206454217235858,1.71802468388708,
5.51036414234011));
#99310=CARTESIAN_POINT('Ctrl Pts',(-1.55645812728861,0.756624656451833,
5.58984142518693));
#99311=CARTESIAN_POINT('Ctrl Pts',(-1.47839964868043,-0.89930885193967,
5.66931870803372));
#99312=CARTESIAN_POINT('Ctrl Pts',(-0.0449224611193922,-1.72937439345709,
5.74879599088053));
#99313=CARTESIAN_POINT('Ctrl Pts',(1.4310732776285,-0.974958136164747,5.82827327372733));
#99314=CARTESIAN_POINT('Ctrl Pts',(1.59179393633893,0.67743703460707,5.90775055657414));
#99315=CARTESIAN_POINT('Ctrl Pts',(0.7293137401282,1.35916011410226,5.96073541180533));
#99316=CARTESIAN_POINT('Ctrl Pts',(0.24921040214603,1.44212566216062,5.98722783942093));
#99317=CARTESIAN_POINT('Ctrl Pts',(-1.46453843780727,0.00118155242986957,
5.12584495415709));
#99318=CARTESIAN_POINT('Ctrl Pts',(-1.46096283466848,-0.406291468589608,
5.14804830642237));
#99319=CARTESIAN_POINT('Ctrl Pts',(-1.28353062640651,-0.816495066456357,
5.17025165868763));
#99320=CARTESIAN_POINT('Ctrl Pts',(-0.981660613063253,-1.08868875643554,
5.19245501095291));
#99321=CARTESIAN_POINT('Ctrl Pts',(-0.621477637885904,-1.41346276096618,
5.21894743856851));
#99322=CARTESIAN_POINT('Ctrl Pts',(-0.0841374835661431,-1.54175752063151,
5.24543986618411));
#99323=CARTESIAN_POINT('Ctrl Pts',(0.383921782776714,-1.41474172471665,
5.27193229379971));
#99324=CARTESIAN_POINT('Ctrl Pts',(0.851981049119571,-1.28772592880178,
5.29842472141532));
#99325=CARTESIAN_POINT('Ctrl Pts',(1.25075942748552,-0.905399577306726,
5.32491714903091));
#99326=CARTESIAN_POINT('Ctrl Pts',(1.39734853185616,-0.443093989891596,
5.35140957664651));
#99327=CARTESIAN_POINT('Ctrl Pts',(1.5439376362268,0.0192115975235344,5.37790200426211));
#99328=CARTESIAN_POINT('Ctrl Pts',(1.43833746660212,0.561496420858736,5.40439443187772));
#99329=CARTESIAN_POINT('Ctrl Pts',(1.12900546275424,0.935012739141861,5.43088685949332));
#99330=CARTESIAN_POINT('Ctrl Pts',(0.819673458906346,1.30852905742499,5.45737928710892));
#99331=CARTESIAN_POINT('Ctrl Pts',(0.306609620835244,1.51327687065604,5.48387171472452));
#99332=CARTESIAN_POINT('Ctrl Pts',(-0.174922949875765,1.45541743936568,
5.51036414234012));
#99333=CARTESIAN_POINT('Ctrl Pts',(-0.333273440429853,1.43639054505928,
5.51907609489341));
#99334=CARTESIAN_POINT('Ctrl Pts',(-0.488214130898924,1.3889652297675,5.5277880474467));
#99335=CARTESIAN_POINT('Ctrl Pts',(-0.632402293996042,1.31836377294842,
5.53649999999999));
#99336=CARTESIAN_POINT('Ctrl Pts',(-0.686152415706132,-0.959598509482516,
1.5365));
#99337=CARTESIAN_POINT('Ctrl Pts',(-0.712494035170421,-0.945273650511668,
1.5365));
#99338=CARTESIAN_POINT('Ctrl Pts',(-0.738199273837341,-0.929906790018379,
1.5365));
#99339=CARTESIAN_POINT('Ctrl Pts',(-0.76319848072749,-0.913511944752561,
1.5365));
#99340=CARTESIAN_POINT('Ctrl Pts',(-0.803527305903368,-0.887063711757967,
1.5365));
#99341=CARTESIAN_POINT('Ctrl Pts',(-0.842020123735519,-0.857943002317074,
1.5365));
#99342=CARTESIAN_POINT('Ctrl Pts',(-0.878605013002918,-0.826447578753258,
1.5365));
#99343=CARTESIAN_POINT('Ctrl Pts',(-0.893209991539167,-0.813874355371944,
1.5365));
#99344=CARTESIAN_POINT('Ctrl Pts',(-0.907510708709607,-0.800922130432144,
1.5365));
#99345=CARTESIAN_POINT('Ctrl Pts',(-0.921501670960182,-0.78760780511351,
1.5365));
#99346=CARTESIAN_POINT('Ctrl Pts',(-0.933569527146362,-0.776123579776924,
1.5365));
#99347=CARTESIAN_POINT('Ctrl Pts',(-0.945411135515606,-0.764365251470628,
1.5365));
#99348=CARTESIAN_POINT('Ctrl Pts',(-0.9569987239283,-0.752368736596883,
1.5365));
#99349=CARTESIAN_POINT('Ctrl Pts',(-0.992167598620615,-0.715958750902441,
1.5365));
#99350=CARTESIAN_POINT('Ctrl Pts',(-1.02503479626171,-0.67732699119571,
1.5365));
#99351=CARTESIAN_POINT('Ctrl Pts',(-1.0555193152036,-0.63679810848881,1.5365));
#99352=CARTESIAN_POINT('Ctrl Pts',(-1.07703618390047,-0.608191632877453,
1.5365));
#99353=CARTESIAN_POINT('Ctrl Pts',(-1.09736563857017,-0.578638841695071,
1.5365));
#99354=CARTESIAN_POINT('Ctrl Pts',(-1.11647108585219,-0.548240703646319,
1.5365));
#99355=CARTESIAN_POINT('Ctrl Pts',(-1.12390764029007,-0.536408611726533,
1.5365));
#99356=CARTESIAN_POINT('Ctrl Pts',(-1.13115866792403,-0.524448342927677,
1.5365));
#99357=CARTESIAN_POINT('Ctrl Pts',(-1.13822167350261,-0.512365491178729,
1.5365));
#99358=CARTESIAN_POINT('Ctrl Pts',(-1.14363503317147,-0.503104727950552,
1.5365));
#99359=CARTESIAN_POINT('Ctrl Pts',(-1.14893488231534,-0.49377706110977,
1.5365));
#99360=CARTESIAN_POINT('Ctrl Pts',(-1.15411691145542,-0.484391843911832,
1.5365));
#99361=CARTESIAN_POINT('Ctrl Pts',(-1.17952890780578,-0.438367960461035,
1.5365));
#99362=CARTESIAN_POINT('Ctrl Pts',(-1.2021374844888,-0.390916630562921,
1.5365));
#99363=CARTESIAN_POINT('Ctrl Pts',(-1.22185604956371,-0.342366499555546,
1.5365));
#99364=CARTESIAN_POINT('Ctrl Pts',(-1.24192204262271,-0.292960947574161,
1.5365));
#99365=CARTESIAN_POINT('Ctrl Pts',(-1.25899605993211,-0.24241663381677,
1.5365));
#99366=CARTESIAN_POINT('Ctrl Pts',(-1.27295041465054,-0.191041522245861,
1.5365));
#99367=CARTESIAN_POINT('Ctrl Pts',(-1.28082576544375,-0.162047202277287,
1.5365));
#99368=CARTESIAN_POINT('Ctrl Pts',(-1.28770675895069,-0.132787650325744,
1.5365));
#99369=CARTESIAN_POINT('Ctrl Pts',(-1.29356400665812,-0.103314695812419,
1.5365));
#99370=CARTESIAN_POINT('Ctrl Pts',(-1.2969812891964,-0.0861193477853134,
1.5365));
#99371=CARTESIAN_POINT('Ctrl Pts',(-1.30005000808393,-0.0688513209636838,
1.5365));
#99372=CARTESIAN_POINT('Ctrl Pts',(-1.30276348910828,-0.0515206690492249,
1.5365));
#99373=CARTESIAN_POINT('Ctrl Pts',(-1.30424656518194,-0.0420484542208913,
1.5365));
#99374=CARTESIAN_POINT('Ctrl Pts',(-1.3056232477231,-0.0325585842976975,
1.5365));
#99375=CARTESIAN_POINT('Ctrl Pts',(-1.30689102145782,-0.023065488585942,
1.5365));
#99376=CARTESIAN_POINT('Ctrl Pts',(-1.31414560403258,0.0312568599885747,
1.5365));
#99377=CARTESIAN_POINT('Ctrl Pts',(-1.31785529058084,0.0857923203720823,
1.5365));
#99378=CARTESIAN_POINT('Ctrl Pts',(-1.31790420900109,0.1402116924761,1.5365));
#99379=CARTESIAN_POINT('Ctrl Pts',(-1.31791152730721,0.148352953421936,
1.5365));
#99380=CARTESIAN_POINT('Ctrl Pts',(-1.31783683331776,0.156491665536181,
1.5365));
#99381=CARTESIAN_POINT('Ctrl Pts',(-1.317679650248,0.164626773622555,1.5365));
#99382=CARTESIAN_POINT('Ctrl Pts',(-1.31666603814062,0.217086902209856,
1.5365));
#99383=CARTESIAN_POINT('Ctrl Pts',(-1.31222643198864,0.269396465505187,
1.5365));
#99384=CARTESIAN_POINT('Ctrl Pts',(-1.30456361513445,0.321337523597355,
1.5365));
#99385=CARTESIAN_POINT('Ctrl Pts',(-1.30051454578202,0.348783428994311,
1.5365));
#99386=CARTESIAN_POINT('Ctrl Pts',(-1.2955646372317,0.37612659768885,1.5365));
#99387=CARTESIAN_POINT('Ctrl Pts',(-1.28973814095309,0.403335224922055,
1.5365));
#99388=CARTESIAN_POINT('Ctrl Pts',(-1.2862415448417,0.419663662396445,1.5365));
#99389=CARTESIAN_POINT('Ctrl Pts',(-1.28242917766058,0.435943645330663,
1.5365));
#99390=CARTESIAN_POINT('Ctrl Pts',(-1.27830564133165,0.452168239721719,
1.5365));
#99391=CARTESIAN_POINT('Ctrl Pts',(-1.27574041647476,0.462261453290118,
1.5365));
#99392=CARTESIAN_POINT('Ctrl Pts',(-1.2730541502057,0.472335075186927,1.5365));
#99393=CARTESIAN_POINT('Ctrl Pts',(-1.27025284985987,0.48237055868,1.5365));
#99394=CARTESIAN_POINT('Ctrl Pts',(-1.25551450272141,0.535169766606186,
1.5365));
#99395=CARTESIAN_POINT('Ctrl Pts',(-1.23757288320391,0.587010386885858,
1.5365));
#99396=CARTESIAN_POINT('Ctrl Pts',(-1.21666787173329,0.637656586978249,
1.5365));
#99397=CARTESIAN_POINT('Ctrl Pts',(-1.19530486219449,0.689412370858058,
1.5365));
#99398=CARTESIAN_POINT('Ctrl Pts',(-1.17084697491721,0.739921779742627,
1.5365));
#99399=CARTESIAN_POINT('Ctrl Pts',(-1.14349524099203,0.788933686107659,
1.5365));
#99400=CARTESIAN_POINT('Ctrl Pts',(-1.12810345611826,0.816514413570401,
1.5365));
#99401=CARTESIAN_POINT('Ctrl Pts',(-1.11179430699787,0.843620855477256,
1.5365));
#99402=CARTESIAN_POINT('Ctrl Pts',(-1.09459665262041,0.870206538635187,
1.5365));
#99403=CARTESIAN_POINT('Ctrl Pts',(-1.08383474902506,0.88684325855539,1.5365));
#99404=CARTESIAN_POINT('Ctrl Pts',(-1.07272481249571,0.903276019161565,
1.5365));
#99405=CARTESIAN_POINT('Ctrl Pts',(-1.06127299753307,0.91949299125179,1.5365));
#99406=CARTESIAN_POINT('Ctrl Pts',(-1.05549186873079,0.927679676483991,
1.5365));
#99407=CARTESIAN_POINT('Ctrl Pts',(-1.04962360295717,0.93581136288618,1.5365));
#99408=CARTESIAN_POINT('Ctrl Pts',(-1.04366892717758,0.943886487236255,
1.5365));
#99409=CARTESIAN_POINT('Ctrl Pts',(-1.0377095980409,0.951967921994928,1.5365));
#99410=CARTESIAN_POINT('Ctrl Pts',(-1.03166885456697,0.95998571466195,1.5365));
#99411=CARTESIAN_POINT('Ctrl Pts',(-1.02554963940643,0.967936312123916,
1.5365));
#99412=CARTESIAN_POINT('Ctrl Pts',(-0.990020557844862,1.01409867417178,
1.5365));
#99413=CARTESIAN_POINT('Ctrl Pts',(-0.951832196594494,1.05802122834032,
1.5365));
#99414=CARTESIAN_POINT('Ctrl Pts',(-0.91120580136671,1.09944292379416,1.5365));
#99415=CARTESIAN_POINT('Ctrl Pts',(-0.869828518644135,1.14163020607782,
1.5365));
#99416=CARTESIAN_POINT('Ctrl Pts',(-0.825921863712725,1.18122453014316,
1.5365));
#99417=CARTESIAN_POINT('Ctrl Pts',(-0.779668622671583,1.21792896816084,
1.5365));
#99418=CARTESIAN_POINT('Ctrl Pts',(-0.73341538163044,1.25463340617853,1.5365));
#99419=CARTESIAN_POINT('Ctrl Pts',(-0.684814997070202,1.28844917107134,
1.5365));
#99420=CARTESIAN_POINT('Ctrl Pts',(-0.634007094575213,1.31904027763685,
1.5365));
#99421=CARTESIAN_POINT('Origin',(-3.28582941601228E-17,0.,1.5365));
#99422=CARTESIAN_POINT('',(-1.4635,-1.79227059055215E-16,1.5365));
#99423=CARTESIAN_POINT('Origin',(0.,0.,1.5365));
#99424=CARTESIAN_POINT('Origin',(0.,0.,1.5365));
#99425=CARTESIAN_POINT('Origin',(0.,0.,1.5));
#99426=CARTESIAN_POINT('Origin',(3.,0.,0.));
#99427=CARTESIAN_POINT('',(-3.,-3.67394039744206E-16,0.));
#99428=CARTESIAN_POINT('Origin',(0.,0.,0.));
#99429=CARTESIAN_POINT('Origin',(0.,0.,0.75));
#99430=CARTESIAN_POINT('',(-2.25,-2.75545529808154E-16,0.75));
#99431=CARTESIAN_POINT('Origin',(0.,0.,6.));
#99507=UNCERTAINTY_MEASURE_WITH_UNIT(LENGTH_MEASURE(0.01),#99527,
'DISTANCE_ACCURACY_VALUE',
'Maximum model space distance between geometric entities at asserted c
onnectivities');
#99508=UNCERTAINTY_MEASURE_WITH_UNIT(LENGTH_MEASURE(0.01),#99527,
'DISTANCE_ACCURACY_VALUE',
'Maximum model space distance between geometric entities at asserted c
onnectivities');
#99525=(
GEOMETRIC_REPRESENTATION_CONTEXT(3)
GLOBAL_UNCERTAINTY_ASSIGNED_CONTEXT((#99507))
GLOBAL_UNIT_ASSIGNED_CONTEXT((#99527,#99529,#99530))
REPRESENTATION_CONTEXT('','3D')
);
#99526=(
GEOMETRIC_REPRESENTATION_CONTEXT(3)
GLOBAL_UNCERTAINTY_ASSIGNED_CONTEXT((#99508))
GLOBAL_UNIT_ASSIGNED_CONTEXT((#99527,#99529,#99530))
REPRESENTATION_CONTEXT('','3D')
);
#99527=(
LENGTH_UNIT()
NAMED_UNIT(*)
SI_UNIT(.MILLI.,.METRE.)
);
#99529=(
NAMED_UNIT(*)
PLANE_ANGLE_UNIT()
SI_UNIT($,.RADIAN.)
);
#99530=(
NAMED_UNIT(*)
SI_UNIT($,.STERADIAN.)
SOLID_ANGLE_UNIT()
);
#99547=SHAPE_DEFINITION_REPRESENTATION(#99564,#99640);
#99564=PRODUCT_DEFINITION_SHAPE('',$,#99658);
#99640=SHAPE_REPRESENTATION('',(#19701),#99525);
#99641=PRODUCT_DEFINITION_CONTEXT('part definition',#99694,'design');
#99658=PRODUCT_DEFINITION('Countersunk screw M3x6',
'Countersunk screw M3x6',#99675,#99641);
#99675=PRODUCT_DEFINITION_FORMATION('',$,#99712);
#99694=APPLICATION_CONTEXT(
'Core Data for Automotive Mechanical Design Process');
#99695=PRODUCT_CONTEXT('part definition',#99694,'mechanical');
#99712=PRODUCT('Countersunk screw M3x6','Countersunk screw M3x6',$,(#99695));
#99725=PRESENTATION_STYLE_ASSIGNMENT((#99738));
#99738=SURFACE_STYLE_USAGE(.BOTH.,#99751);
#99751=SURFACE_SIDE_STYLE('',(#99764));
#99764=SURFACE_STYLE_FILL_AREA(#99777);
#99777=FILL_AREA_STYLE('Screw gray',(#99790));
#99790=FILL_AREA_STYLE_COLOUR('Screw gray',#99803);
#99803=COLOUR_RGB('Screw gray',0.407843137254902,0.447058823529412,0.498039215686275);
ENDSEC;
END-ISO-10303-21;
